ISO-10303-21;
HEADER;
FILE_DESCRIPTION (('STEP AP214'),
    '1' );
FILE_NAME ('left arm.step',
    '2026-10-28T16:30:29',
    ( '' ),
    ( '' ),
    'SwSTEP 2.0',
    'SolidWorks 2025',
    '' );
FILE_SCHEMA (( 'AUTOMOTIVE_DESIGN' ));
ENDSEC;

DATA;
#6=CARTESIAN_POINT ( 'NONE',  ( -16.49999999999998934, 16.00000000000003908, 44.76505905230379767 ) ) ;
#7=CARTESIAN_POINT ( 'NONE',  ( 27.24881022415626575, -213.6786602093778242, 88.60457046541063164 ) ) ;
#15=DIRECTION ( 'NONE',  ( 0.000000000000000000, 1.301042606982607490E-15, -1.000000000000000000 ) ) ;
#17=CARTESIAN_POINT ( 'NONE',  ( 20.98347821072601960, -218.0630240738405519, 87.23510494545232064 ) ) ;
#18=CARTESIAN_POINT ( 'NONE',  ( 20.97288657943079571, -223.0630240738404382, 88.26575131447681599 ) ) ;
#19=CARTESIAN_POINT ( 'NONE',  ( -17.32280336819468047, -61.82280336819459166, 34.82280336819469824 ) ) ;
#21=PRODUCT_DEFINITION_CONTEXT ( 'detailed design', #2454, 'design' ) ;
#22=EDGE_LOOP ( 'NONE', ( #2076, #4866, #387, #2753, #42, #1784, #2773 ) ) ;
#36=LINE ( 'NONE', #2385, #2482 ) ;
#37=EDGE_CURVE ( 'NONE', #4344, #2575, #5917, .T. ) ;
#42=ORIENTED_EDGE ( 'NONE', *, *, #4968, .F. ) ;
#48=ORIENTED_EDGE ( 'NONE', *, *, #3226, .T. ) ;
#51=DIRECTION ( 'NONE',  ( -1.084202172485505174E-16, 0.000000000000000000, 1.000000000000000000 ) ) ;
#62=DIRECTION ( 'NONE',  ( 0.000000000000000000, 0.000000000000000000, 1.000000000000000000 ) ) ;
#63=CARTESIAN_POINT ( 'NONE',  ( 21.48754873573582813, -218.0630240738405803, 84.27726093503913773 ) ) ;
#75=AXIS2_PLACEMENT_3D ( 'NONE', #6050, #2005, #4940 ) ;
#81=DIRECTION ( 'NONE',  ( -1.000000000000000000, 0.000000000000000000, -7.663350976776343357E-46 ) ) ;
#89=ORIENTED_EDGE ( 'NONE', *, *, #875, .F. ) ;
#93=CARTESIAN_POINT ( 'NONE',  ( 17.75187451922245430, -223.0194114314941203, 73.26959217102432831 ) ) ;
#95=SHAPE_DEFINITION_REPRESENTATION ( #6712, #867 ) ;
#105=VERTEX_POINT ( 'NONE', #3335 ) ;
#130=CARTESIAN_POINT ( 'NONE',  ( 27.04900473833201957, -225.0595978535630479, 79.55554317441176693 ) ) ;
#142=CARTESIAN_POINT ( 'NONE',  ( -16.49999999999996447, -57.68629150101509850, 30.68629150101520509 ) ) ;
#148=LINE ( 'NONE', #4110, #1043 ) ;
#159=CARTESIAN_POINT ( 'NONE',  ( -11.51602904742824762, -108.8525495989622556, 36.85254959896237636 ) ) ;
#162=VERTEX_POINT ( 'NONE', #7062 ) ;
#164=CARTESIAN_POINT ( 'NONE',  ( 10.17910001414514731, -221.3248423084432943, 72.81553374298380277 ) ) ;
#165=ORIENTED_EDGE ( 'NONE', *, *, #3061, .F. ) ;
#167=LINE ( 'NONE', #6090, #918 ) ;
#171=EDGE_CURVE ( 'NONE', #5235, #6417, #2962, .T. ) ;
#179=( BOUNDED_CURVE ( )  B_SPLINE_CURVE ( 3, ( #5830, #5717, #554, #2902 ),
 .UNSPECIFIED., .F., .T. ) 
 B_SPLINE_CURVE_WITH_KNOTS ( ( 4, 4 ),
 ( 1.637599047967249533, 2.356194490192343061 ),
 .UNSPECIFIED. ) 
 CURVE ( )  GEOMETRIC_REPRESENTATION_ITEM ( )  RATIONAL_B_SPLINE_CURVE ( ( 1.000000000000000000, 0.9574293250827446977, 0.9574293250827446977, 1.000000000000000000 ) ) 
 REPRESENTATION_ITEM ( '' )  );
#183=LINE ( 'NONE', #5993, #3215 ) ;
#199=CARTESIAN_POINT ( 'NONE',  ( -21.50000000000000000, -215.0630240738404950, 71.13768460387146320 ) ) ;
#203=ORIENTED_EDGE ( 'NONE', *, *, #3523, .T. ) ;
#206=CARTESIAN_POINT ( 'NONE',  ( 27.00607124224622169, -226.9703646923684062, 80.02312588464758392 ) ) ;
#212=CARTESIAN_POINT ( 'NONE',  ( -21.50000000000000000, -215.0630240738404950, 71.13768460387146320 ) ) ;
#236=LINE ( 'NONE', #5475, #4353 ) ;
#237=CARTESIAN_POINT ( 'NONE',  ( 27.16044999292957840, -220.0996966972330995, 78.34180846956240885 ) ) ;
#238=VERTEX_POINT ( 'NONE', #3137 ) ;
#250=ORIENTED_EDGE ( 'NONE', *, *, #171, .T. ) ;
#261=ORIENTED_EDGE ( 'NONE', *, *, #5274, .T. ) ;
#263=CARTESIAN_POINT ( 'NONE',  ( -10.49999999999996803, -60.68629150101523351, -11.31370849898472031 ) ) ;
#274=ORIENTED_EDGE ( 'NONE', *, *, #4877, .F. ) ;
#279=DIRECTION ( 'NONE',  ( 0.000000000000000000, 0.000000000000000000, 1.000000000000000000 ) ) ;
#288=ORIENTED_EDGE ( 'NONE', *, *, #3333, .T. ) ;
#304=DIRECTION ( 'NONE',  ( 3.379803290564628095E-16, 1.221245327087672392E-15, -1.000000000000000000 ) ) ;
#309=CIRCLE ( 'NONE', #7190, 5.999999999999999112 ) ;
#313=CARTESIAN_POINT ( 'NONE',  ( 21.50000000000000000, 6.938893903907228378E-15, -16.00000000000001421 ) ) ;
#318=DIRECTION ( 'NONE',  ( -1.000000000000000000, 1.294224922628222493E-31, -1.078147950931789264E-16 ) ) ;
#324=CARTESIAN_POINT ( 'NONE',  ( -18.50000000000000355, 16.00000000000006750, 32.26953873476012546 ) ) ;
#330=DIRECTION ( 'NONE',  ( -3.379803290564627601E-16, 0.000000000000000000, 1.000000000000000000 ) ) ;
#332=CARTESIAN_POINT ( 'NONE',  ( -16.50000000000000711, -214.0630240738404382, 94.50428307177961074 ) ) ;
#338=DIRECTION ( 'NONE',  ( -1.000000000000000000, 0.000000000000000000, -7.663350976776343357E-46 ) ) ;
#339=CARTESIAN_POINT ( 'NONE',  ( -16.50000000000000711, -223.0630240738404666, 96.09122589815579829 ) ) ;
#341=ORIENTED_EDGE ( 'NONE', *, *, #5136, .F. ) ;
#362=CARTESIAN_POINT ( 'NONE',  ( -21.50000000000000000, -223.0630240738404666, 96.09122589815579829 ) ) ;
#370=VECTOR ( 'NONE', #1803, 1000.000000000000000 ) ;
#372=ORIENTED_EDGE ( 'NONE', *, *, #3640, .F. ) ;
#373=LINE ( 'NONE', #6957, #4602 ) ;
#384=ORIENTED_EDGE ( 'NONE', *, *, #1937, .F. ) ;
#387=ORIENTED_EDGE ( 'NONE', *, *, #1165, .F. ) ;
#390=EDGE_LOOP ( 'NONE', ( #4887, #963, #5814, #6487, #1201, #1973, #2378, #1958, #3679, #4178 ) ) ;
#397=ORIENTED_EDGE ( 'NONE', *, *, #2841, .F. ) ;
#435=ORIENTED_EDGE ( 'NONE', *, *, #7404, .T. ) ;
#440=ORIENTED_EDGE ( 'NONE', *, *, #3673, .F. ) ;
#442=PLANE ( 'NONE',  #948 ) ;
#443=CARTESIAN_POINT ( 'NONE',  ( -16.49999999999996447, -39.68629150101519087, 15.99999999999998579 ) ) ;
#449=EDGE_CURVE ( 'NONE', #3729, #4344, #2629, .T. ) ;
#462=ORIENTED_EDGE ( 'NONE', *, *, #2114, .F. ) ;
#473=ADVANCED_FACE ( 'NONE', ( #2054 ), #6822, .T. ) ;
#475=ADVANCED_FACE ( 'NONE', ( #6202 ), #7356, .F. ) ;
#479=CARTESIAN_POINT ( 'NONE',  ( 13.86971907638974244, -223.0630240738404382, 73.89376335044022426 ) ) ;
#490=ORIENTED_EDGE ( 'NONE', *, *, #3084, .F. ) ;
#503=DIRECTION ( 'NONE',  ( 1.000000000000000000, 0.000000000000000000, -7.663350976776344912E-46 ) ) ;
#504=CARTESIAN_POINT ( 'NONE',  ( 26.99871551551753868, -224.9174535703052129, 90.83998408137779279 ) ) ;
#513=ADVANCED_FACE ( 'NONE', ( #7393 ), #1436, .T. ) ;
#518=CARTESIAN_POINT ( 'NONE',  ( 10.47314606205195631, -223.0630240738404666, 96.09122589815579829 ) ) ;
#543=CARTESIAN_POINT ( 'NONE',  ( 10.43756829269602804, -222.2597742987530012, 95.94959129055985159 ) ) ;
#551=VERTEX_POINT ( 'NONE', #1009 ) ;
#554=CARTESIAN_POINT ( 'NONE',  ( -20.54184453752627348, -110.0418445375260603, 38.04184453752623085 ) ) ;
#556=LINE ( 'NONE', #1790, #3266 ) ;
#557=CARTESIAN_POINT ( 'NONE',  ( 21.48772344548951452, -218.0630240738405234, 82.75416678248926416 ) ) ;
#559=CARTESIAN_POINT ( 'NONE',  ( -19.15685424949238325, -63.65685424949226245, 36.65685424949236193 ) ) ;
#578=VERTEX_POINT ( 'NONE', #3521 ) ;
#583=CARTESIAN_POINT ( 'NONE',  ( 17.66745985056437362, -212.4343899438515848, 94.21711093295448336 ) ) ;
#586=PRODUCT_CONTEXT ( 'NONE', #3644, 'mechanical' ) ;
#590=CARTESIAN_POINT ( 'NONE',  ( 21.50000000000000000, -223.0630240738404666, 96.09122589815579829 ) ) ;
#594=CARTESIAN_POINT ( 'NONE',  ( 20.85637474134628988, -223.0630240738404098, 88.61643661315291354 ) ) ;
#621=CARTESIAN_POINT ( 'NONE',  ( 17.82928583850155135, -223.3951688904013224, 96.14979199081716388 ) ) ;
#628=VERTEX_POINT ( 'NONE', #6978 ) ;
#630=DIRECTION ( 'NONE',  ( 0.000000000000000000, -1.000000000000000000, -1.221245327087672392E-15 ) ) ;
#633=CARTESIAN_POINT ( 'NONE',  ( 18.83797478939531445, -218.0630240738405234, 91.18492895007960897 ) ) ;
#637=UNCERTAINTY_MEASURE_WITH_UNIT (LENGTH_MEASURE( 1.000000000000000082E-05 ), #5446, 'distance_accuracy_value', 'NONE');
#639=AXIS2_PLACEMENT_3D ( 'NONE', #6879, #1719, #7491 ) ;
#652=CARTESIAN_POINT ( 'NONE',  ( -10.49999999999998224, -99.90626354475340065, 72.90626354475362803 ) ) ;
#661=CARTESIAN_POINT ( 'NONE',  ( 10.48785751550376766, -228.1620966263577657, 74.64757051591513459 ) ) ;
#666=ORIENTED_EDGE ( 'NONE', *, *, #3367, .T. ) ;
#674=CARTESIAN_POINT ( 'NONE',  ( 19.00163867460213396, -218.0630240738404666, 76.36460184284905495 ) ) ;
#687=VERTEX_POINT ( 'NONE', #3637 ) ;
#688=LINE ( 'NONE', #1876, #3153 ) ;
#698=VECTOR ( 'NONE', #1441, 1000.000000000000000 ) ;
#699=LINE ( 'NONE', #6, #2270 ) ;
#700=CARTESIAN_POINT ( 'NONE',  ( 27.24881022415653220, -216.1672007404107205, 77.37948953034242550 ) ) ;
#705=AXIS2_PLACEMENT_3D ( 'NONE', #885, #2584, #4943 ) ;
#717=DIRECTION ( 'NONE',  ( 7.006492321624086910E-46, -1.221245327087672392E-15, 1.000000000000000000 ) ) ;
#724=FACE_OUTER_BOUND ( 'NONE', #5224, .T. ) ;
#731=AXIS2_PLACEMENT_3D ( 'NONE', #6131, #2590, #3794 ) ;
#733=CARTESIAN_POINT ( 'NONE',  ( 27.25616595088856542, -215.8398321358105250, 77.29937933778069237 ) ) ;
#752=CARTESIAN_POINT ( 'NONE',  ( -21.49436104581528184, -113.9621117585879944, 41.96211175858819331 ) ) ;
#763=CARTESIAN_POINT ( 'NONE',  ( -10.49999999999997513, -104.2695387347598057, 32.26953873475996204 ) ) ;
#776=DIRECTION ( 'NONE',  ( 0.000000000000000000, 0.000000000000000000, 1.000000000000000000 ) ) ;
#787=CIRCLE ( 'NONE', #5834, 5.999999999999999112 ) ;
#793=CARTESIAN_POINT ( 'NONE',  ( -21.50000000000000000, -125.0933926253236308, 30.46597562735434295 ) ) ;
#807=ORIENTED_EDGE ( 'NONE', *, *, #4249, .F. ) ;
#809=CARTESIAN_POINT ( 'NONE',  ( 10.01709100512437267, -217.7372475398855727, 71.85424062197864714 ) ) ;
#828=ORIENTED_EDGE ( 'NONE', *, *, #1061, .F. ) ;
#833=EDGE_CURVE ( 'NONE', #7034, #6433, #7263, .T. ) ;
#838=ORIENTED_EDGE ( 'NONE', *, *, #4968, .T. ) ;
#844=ORIENTED_EDGE ( 'NONE', *, *, #4014, .T. ) ;
#851=ORIENTED_EDGE ( 'NONE', *, *, #1917, .F. ) ;
#852=LINE ( 'NONE', #1941, #3097 ) ;
#861=FACE_OUTER_BOUND ( 'NONE', #6349, .T. ) ;
#867=SHAPE_REPRESENTATION ( 'left arm', ( #1914 ), #5724 ) ;
#870=VECTOR ( 'NONE', #5276, 1000.000000000000114 ) ;
#875=EDGE_CURVE ( 'NONE', #1532, #4506, #4939, .T. ) ;
#877=VERTEX_POINT ( 'NONE', #2654 ) ;
#885=CARTESIAN_POINT ( 'NONE',  ( 21.50000000000000000, 0.000000000000000000, 0.000000000000000000 ) ) ;
#894=ORIENTED_EDGE ( 'NONE', *, *, #5077, .F. ) ;
#904=CARTESIAN_POINT ( 'NONE',  ( 21.50000000000000000, -49.37258300203047412, -15.99999999999998579 ) ) ;
#905=AXIS2_PLACEMENT_3D ( 'NONE', #6934, #503, #3973 ) ;
#910=CARTESIAN_POINT ( 'NONE',  ( -10.49999999999997513, -59.26953873475991230, 32.26953873476001888 ) ) ;
#918=VECTOR ( 'NONE', #3165, 1000.000000000000000 ) ;
#926=ORIENTED_EDGE ( 'NONE', *, *, #1410, .F. ) ;
#934=CARTESIAN_POINT ( 'NONE',  ( 21.50000000000000000, 6.938893903907228378E-15, -16.00000000000001421 ) ) ;
#948=AXIS2_PLACEMENT_3D ( 'NONE', #3369, #5104, #1127 ) ;
#951=DIRECTION ( 'NONE',  ( 1.000000000000000000, -1.294224922628222493E-31, 1.078147950931789264E-16 ) ) ;
#952=CYLINDRICAL_SURFACE ( 'NONE', #2411, 8.000000000000007105 ) ;
#955=ORIENTED_EDGE ( 'NONE', *, *, #4014, .F. ) ;
#957=( BOUNDED_CURVE ( )  B_SPLINE_CURVE ( 3, ( #2661, #2086, #6816, #1431 ),
 .UNSPECIFIED., .F., .T. ) 
 B_SPLINE_CURVE_WITH_KNOTS ( ( 4, 4 ),
 ( 3.839724354387530791, 4.329963465791603738 ),
 .UNSPECIFIED. ) 
 CURVE ( )  GEOMETRIC_REPRESENTATION_ITEM ( )  RATIONAL_B_SPLINE_CURVE ( ( 1.000000000000000000, 0.9800722126984333649, 0.9800722126984333649, 1.000000000000000000 ) ) 
 REPRESENTATION_ITEM ( '' )  );
#963=ORIENTED_EDGE ( 'NONE', *, *, #1690, .T. ) ;
#974=CARTESIAN_POINT ( 'NONE',  ( -16.49999999999996803, 16.00000000000012079, -15.99999999999995914 ) ) ;
#977=DIRECTION ( 'NONE',  ( 0.000000000000000000, -1.000000000000000000, -1.221245327087672392E-15 ) ) ;
#985=AXIS2_PLACEMENT_3D ( 'NONE', #793, #6172, #3145 ) ;
#989=FACE_OUTER_BOUND ( 'NONE', #3206, .T. ) ;
#1002=EDGE_CURVE ( 'NONE', #2056, #3791, #7485, .T. ) ;
#1009=CARTESIAN_POINT ( 'NONE',  ( -16.49999999999996447, -57.68629150101509850, 30.68629150101520509 ) ) ;
#1013=LINE ( 'NONE', #2295, #5131 ) ;
#1021=ORIENTED_EDGE ( 'NONE', *, *, #1002, .F. ) ;
#1029=DIRECTION ( 'NONE',  ( 2.389881825834862305E-16, 0.7071067811865465735, -0.7071067811865485719 ) ) ;
#1030=VECTOR ( 'NONE', #6185, 1000.000000000000000 ) ;
#1043=VECTOR ( 'NONE', #2374, 1000.000000000000000 ) ;
#1051=ORIENTED_EDGE ( 'NONE', *, *, #7061, .F. ) ;
#1058=CARTESIAN_POINT ( 'NONE',  ( 19.22919491717249940, -223.0630240738404666, 77.71142956833992343 ) ) ;
#1059=CARTESIAN_POINT ( 'NONE',  ( -21.48215622306531003, -113.7796841263388501, 41.77968412633906325 ) ) ;
#1061=EDGE_CURVE ( 'NONE', #1926, #6198, #4197, .T. ) ;
#1076=DIRECTION ( 'NONE',  ( 0.000000000000000000, -1.000000000000000000, -1.221245327087672392E-15 ) ) ;
#1079=PLANE ( 'NONE',  #2524 ) ;
#1080=ORIENTED_EDGE ( 'NONE', *, *, #6060, .T. ) ;
#1089=ORIENTED_EDGE ( 'NONE', *, *, #2261, .F. ) ;
#1092=CARTESIAN_POINT ( 'NONE',  ( -10.49999999999997513, 16.00000000000006750, 32.26953873476009704 ) ) ;
#1094=CARTESIAN_POINT ( 'NONE',  ( 11.00280363943375228, -223.0630240738404382, 73.28127814332052026 ) ) ;
#1097=EDGE_LOOP ( 'NONE', ( #288, #435, #7329, #203, #5572, #1606 ) ) ;
#1098=EDGE_LOOP ( 'NONE', ( #1806, #3086, #4692, #894 ) ) ;
#1099=CIRCLE ( 'NONE', #1844, 6.000000000000000000 ) ;
#1105=DIRECTION ( 'NONE',  ( 1.000000000000000000, 0.000000000000000000, 7.663350976776343357E-46 ) ) ;
#1107=CIRCLE ( 'NONE', #6397, 6.000000000000000000 ) ;
#1123=EDGE_CURVE ( 'NONE', #2955, #4378, #5353, .T. ) ;
#1127=DIRECTION ( 'NONE',  ( -0.7660444431189622483, 1.387778780781445984E-17, 0.6427876096865581257 ) ) ;
#1130=DIRECTION ( 'NONE',  ( -1.000000000000000000, 0.000000000000000000, -7.663350976776343357E-46 ) ) ;
#1131=CARTESIAN_POINT ( 'NONE',  ( 14.77760111023792255, -218.0630240738404950, 73.00051268027513629 ) ) ;
#1133=CARTESIAN_POINT ( 'NONE',  ( 14.21833974672536449, -223.0630240738404950, 74.02270760457069798 ) ) ;
#1134=CARTESIAN_POINT ( 'NONE',  ( -21.49999999999998934, -67.16361968246707193, 40.16361968246722824 ) ) ;
#1143=EDGE_CURVE ( 'NONE', #1669, #4326, #6150, .T. ) ;
#1153=EDGE_CURVE ( 'NONE', #2279, #4312, #4817, .T. ) ;
#1157=CARTESIAN_POINT ( 'NONE',  ( 10.51728042240002914, -224.0594585235269562, 96.26692417614292197 ) ) ;
#1165=EDGE_CURVE ( 'NONE', #7550, #687, #4238, .T. ) ;
#1173=CARTESIAN_POINT ( 'NONE',  ( 12.10006130380613243, -223.0630240738404382, 73.39180178971804480 ) ) ;
#1177=ORIENTED_EDGE ( 'NONE', *, *, #1495, .F. ) ;
#1178=DIRECTION ( 'NONE',  ( 0.000000000000000000, 0.000000000000000000, -1.000000000000000000 ) ) ;
#1180=CARTESIAN_POINT ( 'NONE',  ( -16.49999999999996803, -49.37258300203047412, -16.00000000000004263 ) ) ;
#1187=DIRECTION ( 'NONE',  ( -1.000000000000000000, 0.000000000000000000, -7.663350976776343357E-46 ) ) ;
#1188=ORIENTED_EDGE ( 'NONE', *, *, #1143, .T. ) ;
#1194=DIRECTION ( 'NONE',  ( 0.000000000000000000, -1.000000000000000000, -1.221245327087672392E-15 ) ) ;
#1195=CARTESIAN_POINT ( 'NONE',  ( 17.83909347413333890, -224.0594585235269562, 96.26692417614293618 ) ) ;
#1201=ORIENTED_EDGE ( 'NONE', *, *, #2873, .T. ) ;
#1202=MANIFOLD_SOLID_BREP ( 'Fillet3', #4556 ) ;
#1203=CARTESIAN_POINT ( 'NONE',  ( 21.50000000000000000, -218.0630240738404382, 71.94153218116483117 ) ) ;
#1209=CARTESIAN_POINT ( 'NONE',  ( 19.52861056693573971, -218.0630240738404950, 90.29964924649102898 ) ) ;
#1210=CARTESIAN_POINT ( 'NONE',  ( 15.94411230092104859, -223.0630240738404382, 94.62561961047832426 ) ) ;
#1211=CARTESIAN_POINT ( 'NONE',  ( -18.84314575050759188, -63.34314575050751017, 36.34314575050759544 ) ) ;
#1235=CARTESIAN_POINT ( 'NONE',  ( 26.99135978879997566, -225.2480063162099952, 90.90573154067851647 ) ) ;
#1240=CARTESIAN_POINT ( 'NONE',  ( -13.49999999999999822, -223.0630240738404382, 73.28127814332047762 ) ) ;
#1241=VERTEX_POINT ( 'NONE', #199 ) ;
#1244=DIRECTION ( 'NONE',  ( -8.758115402030108249E-46, -0.1736481776669305255, -0.9848077530122081313 ) ) ;
#1248=CARTESIAN_POINT ( 'NONE',  ( 18.18549846063790909, -218.0630240738405519, 91.87109893316912235 ) ) ;
#1257=CARTESIAN_POINT ( 'NONE',  ( 10.25168462842736261, -218.0630240738404950, 95.20959099461346398 ) ) ;
#1259=VERTEX_POINT ( 'NONE', #3154 ) ;
#1266=CARTESIAN_POINT ( 'NONE',  ( -10.49999999999998224, -106.6736682753135739, 34.67366827531366624 ) ) ;
#1273=CARTESIAN_POINT ( 'NONE',  ( 10.10580595754474764, -219.7017882839730873, 72.38063772785488936 ) ) ;
#1274=ORIENTED_EDGE ( 'NONE', *, *, #2007, .F. ) ;
#1284=CARTESIAN_POINT ( 'NONE',  ( 21.50000000000000000, -49.37258300203045280, -2.775557561562891351E-14 ) ) ;
#1286=CARTESIAN_POINT ( 'NONE',  ( -19.15685424949238680, -108.6568542494921701, 36.65685424949233351 ) ) ;
#1313=CARTESIAN_POINT ( 'NONE',  ( 17.66745985056476798, -217.4114710059388926, 71.76694906279428210 ) ) ;
#1333=ORIENTED_EDGE ( 'NONE', *, *, #2440, .T. ) ;
#1334=ADVANCED_FACE ( 'NONE', ( #4880 ), #4803, .F. ) ;
#1342=EDGE_CURVE ( 'NONE', #2172, #3560, #2372, .T. ) ;
#1351=VECTOR ( 'NONE', #7324, 1000.000000000000000 ) ;
#1361=EDGE_CURVE ( 'NONE', #5964, #3162, #7140, .T. ) ;
#1364=CARTESIAN_POINT ( 'NONE',  ( -16.50000000000001066, 15.99999999999998579, 96.09122589815608251 ) ) ;
#1374=( LENGTH_UNIT ( ) NAMED_UNIT ( * ) SI_UNIT ( .MILLI., .METRE. ) );
#1380=CARTESIAN_POINT ( 'NONE',  ( 17.80066350777958917, -226.2606222968801433, 74.13807200489549132 ) ) ;
#1384=ORIENTED_EDGE ( 'NONE', *, *, #3640, .T. ) ;
#1394=CYLINDRICAL_SURFACE ( 'NONE', #731, 6.000000000000000000 ) ;
#1404=CARTESIAN_POINT ( 'NONE',  ( -16.50000000000000000, -105.5631177942458265, 67.24940929526127320 ) ) ;
#1410=EDGE_CURVE ( 'NONE', #3211, #7034, #5635, .T. ) ;
#1412=ORIENTED_EDGE ( 'NONE', *, *, #1975, .F. ) ;
#1418=DIRECTION ( 'NONE',  ( 0.000000000000000000, -1.000000000000000000, -1.221245327087672392E-15 ) ) ;
#1424=CARTESIAN_POINT ( 'NONE',  ( 10.00237955168408632, -217.4114710059382958, 71.76694906279443842 ) ) ;
#1425=ORIENTED_EDGE ( 'NONE', *, *, #4295, .F. ) ;
#1429=CARTESIAN_POINT ( 'NONE',  ( 21.50000000000000000, -120.9522879036832848, 45.92078884797942351 ) ) ;
#1431=CARTESIAN_POINT ( 'NONE',  ( -15.92209785380265608, -113.7796841263388501, 41.77968412633906325 ) ) ;
#1436=CYLINDRICAL_SURFACE ( 'NONE', #5660, 8.000000000000014211 ) ;
#1441=DIRECTION ( 'NONE',  ( -1.000000000000000000, 0.000000000000000000, -7.663350976776343357E-46 ) ) ;
#1447=LINE ( 'NONE', #904, #7007 ) ;
#1448=EDGE_LOOP ( 'NONE', ( #7159, #6116, #7543, #6796, #5808, #851, #7113, #4585 ) ) ;
#1450=PLANE ( 'NONE',  #4761 ) ;
#1478=DIRECTION ( 'NONE',  ( 0.000000000000000000, -1.000000000000000000, 0.000000000000000000 ) ) ;
#1479=AXIS2_PLACEMENT_3D ( 'NONE', #4320, #2004, #5045 ) ;
#1481=ORIENTED_EDGE ( 'NONE', *, *, #3523, .F. ) ;
#1495=EDGE_CURVE ( 'NONE', #4506, #5789, #5565, .T. ) ;
#1496=CARTESIAN_POINT ( 'NONE',  ( -16.49999999999996447, -49.37258300203045280, 5.999999999999974243 ) ) ;
#1501=DIRECTION ( 'NONE',  ( 0.000000000000000000, -1.000000000000000000, -5.551115123125783935E-17 ) ) ;
#1518=CARTESIAN_POINT ( 'NONE',  ( 13.02230825830123173, -218.0630240738405519, 72.24324488657181575 ) ) ;
#1519=FACE_BOUND ( 'NONE', #2491, .T. ) ;
#1520=VECTOR ( 'NONE', #1076, 1000.000000000000000 ) ;
#1532=VERTEX_POINT ( 'NONE', #6675 ) ;
#1539=EDGE_LOOP ( 'NONE', ( #4296, #1080, #6036, #6386 ) ) ;
#1543=DIRECTION ( 'NONE',  ( 7.225445206674839578E-46, -5.551115123125783935E-17, 1.000000000000000000 ) ) ;
#1561=DIRECTION ( 'NONE',  ( 1.000000000000000000, 0.000000000000000000, -7.663350976776344912E-46 ) ) ;
#1568=DIRECTION ( 'NONE',  ( 1.311910807449311619E-31, 1.000000000000000000, 0.000000000000000000 ) ) ;
#1573=ADVANCED_FACE ( 'NONE', ( #6285 ), #5212, .F. ) ;
#1585=CARTESIAN_POINT ( 'NONE',  ( 10.47314606205195631, -223.0630240738404666, 96.09122589815579829 ) ) ;
#1589=CARTESIAN_POINT ( 'NONE',  ( -12.50000000000001066, -218.0630240738404950, 95.20959099461346398 ) ) ;
#1598=EDGE_CURVE ( 'NONE', #7269, #105, #4527, .T. ) ;
#1605=AXIS2_PLACEMENT_3D ( 'NONE', #2810, #4587, #4085 ) ;
#1606=ORIENTED_EDGE ( 'NONE', *, *, #1917, .T. ) ;
#1608=ADVANCED_FACE ( 'NONE', ( #5756 ), #6408, .F. ) ;
#1612=VECTOR ( 'NONE', #304, 1000.000000000000000 ) ;
#1615=ORIENTED_EDGE ( 'NONE', *, *, #6120, .T. ) ;
#1623=DIRECTION ( 'NONE',  ( -1.000000000000000000, 0.000000000000000000, -7.663350976776343357E-46 ) ) ;
#1627=CARTESIAN_POINT ( 'NONE',  ( 21.47795444953126420, -223.0630240738404382, 83.13617250284077898 ) ) ;
#1639=CARTESIAN_POINT ( 'NONE',  ( -13.64230087749234599, -65.63670350735179682, 38.63670350735190340 ) ) ;
#1646=ORIENTED_EDGE ( 'NONE', *, *, #3367, .F. ) ;
#1661=CARTESIAN_POINT ( 'NONE',  ( 10.33013951010423170, -219.8343230396699823, 95.52191879319022405 ) ) ;
#1668=ORIENTED_EDGE ( 'NONE', *, *, #1947, .F. ) ;
#1669=VERTEX_POINT ( 'NONE', #7554 ) ;
#1670=EDGE_CURVE ( 'NONE', #105, #7581, #1013, .T. ) ;
#1680=ADVANCED_FACE ( 'NONE', ( #6982 ), #442, .F. ) ;
#1682=CARTESIAN_POINT ( 'NONE',  ( 11.55538789554288037, -218.0630240738405519, 71.94153218116487380 ) ) ;
#1690=EDGE_CURVE ( 'NONE', #3560, #7581, #179, .T. ) ;
#1696=ORIENTED_EDGE ( 'NONE', *, *, #3608, .T. ) ;
#1699=CARTESIAN_POINT ( 'NONE',  ( 10.25759302228802738, -223.0630240738404382, 73.28127814332047762 ) ) ;
#1713=ORIENTED_EDGE ( 'NONE', *, *, #7061, .T. ) ;
#1719=DIRECTION ( 'NONE',  ( -1.000000000000000000, 1.294224922628222493E-31, -1.078147950931789264E-16 ) ) ;
#1728=ADVANCED_FACE ( 'NONE', ( #6521 ), #6014, .F. ) ;
#1732=ADVANCED_FACE ( 'NONE', ( #4179 ), #1939, .F. ) ;
#1736=CARTESIAN_POINT ( 'NONE',  ( 10.00237955168283044, -212.4343899438498511, 94.21711093295958506 ) ) ;
#1746=AXIS2_PLACEMENT_3D ( 'NONE', #3171, #1974, #6669 ) ;
#1749=CARTESIAN_POINT ( 'NONE',  ( 0.000000000000000000, 0.000000000000000000, 0.000000000000000000 ) ) ;
#1751=CARTESIAN_POINT ( 'NONE',  ( 20.79427630190120269, -223.0630240738404950, 88.78961924518958426 ) ) ;
#1755=DIRECTION ( 'NONE',  ( 1.000000000000000000, 0.000000000000000000, 7.663350976776343357E-46 ) ) ;
#1762=DIRECTION ( 'NONE',  ( 0.000000000000000000, 0.000000000000000000, 1.000000000000000000 ) ) ;
#1767=ORIENTED_EDGE ( 'NONE', *, *, #7237, .F. ) ;
#1784=ORIENTED_EDGE ( 'NONE', *, *, #3041, .F. ) ;
#1790=CARTESIAN_POINT ( 'NONE',  ( 21.50000000000000000, -99.90626354475340065, 72.90626354475362803 ) ) ;
#1791=CARTESIAN_POINT ( 'NONE',  ( 10.25168462842736261, -218.0630240738404950, 95.20959099461346398 ) ) ;
#1792=CARTESIAN_POINT ( 'NONE',  ( 16.21315755988861440, -223.0630240738403813, 74.98638948672413562 ) ) ;
#1793=CARTESIAN_POINT ( 'NONE',  ( -20.67719663180526624, -65.17719663180515965, 38.17719663180528045 ) ) ;
#1803=DIRECTION ( 'NONE',  ( 0.000000000000000000, -1.000000000000000000, -1.221245327087672392E-15 ) ) ;
#1806=ORIENTED_EDGE ( 'NONE', *, *, #2983, .T. ) ;
#1808=VECTOR ( 'NONE', #4152, 1000.000000000000000 ) ;
#1815=EDGE_LOOP ( 'NONE', ( #1089, #7121, #4206, #1412, #4899, #6208, #3157 ) ) ;
#1816=AXIS2_PLACEMENT_3D ( 'NONE', #590, #1244, #1861 ) ;
#1817=ORIENTED_EDGE ( 'NONE', *, *, #2873, .F. ) ;
#1840=CARTESIAN_POINT ( 'NONE',  ( -15.92209785380265608, -113.7796841263388501, 41.77968412633906325 ) ) ;
#1844=AXIS2_PLACEMENT_3D ( 'NONE', #7024, #7138, #1868 ) ;
#1851=EDGE_CURVE ( 'NONE', #2809, #4322, #6485, .T. ) ;
#1853=CARTESIAN_POINT ( 'NONE',  ( 17.76462208873361348, -223.8662738488898185, 73.49650827185845969 ) ) ;
#1861=DIRECTION ( 'NONE',  ( -1.751623080406021728E-46, 0.9848077530122081313, -0.1736481776669305255 ) ) ;
#1864=DIRECTION ( 'NONE',  ( 1.000000000000000000, 0.000000000000000000, 0.000000000000000000 ) ) ;
#1866=CARTESIAN_POINT ( 'NONE',  ( 13.22237817618507805, -218.0630240738405234, 94.81205485192671745 ) ) ;
#1868=DIRECTION ( 'NONE',  ( 0.000000000000000000, 0.000000000000000000, 1.000000000000000000 ) ) ;
#1869=DIRECTION ( 'NONE',  ( -1.000000000000000000, 0.000000000000000000, -7.663350976776343357E-46 ) ) ;
#1875=ORIENTED_EDGE ( 'NONE', *, *, #4005, .T. ) ;
#1876=CARTESIAN_POINT ( 'NONE',  ( -16.49999999999996803, 16.00000000000006395, 30.68629150101531877 ) ) ;
#1877=DIRECTION ( 'NONE',  ( 0.000000000000000000, 0.000000000000000000, 1.000000000000000000 ) ) ;
#1879=ADVANCED_FACE ( 'NONE', ( #5018 ), #2009, .T. ) ;
#1888=CARTESIAN_POINT ( 'NONE',  ( 27.14230383934499002, -220.9072961629242116, 78.53943569403831759 ) ) ;
#1889=ADVANCED_FACE ( 'NONE', ( #5518 ), #3202, .F. ) ;
#1893=CIRCLE ( 'NONE', #4977, 15.99999999999999645 ) ;
#1901=SHAPE_REPRESENTATION_RELATIONSHIP ( 'NONE' , 'NONE' ,  #867, #7208 ) ;
#1914=AXIS2_PLACEMENT_3D ( 'NONE', #1749, #62, #1864 ) ;
#1917=EDGE_CURVE ( 'NONE', #7550, #6856, #4583, .T. ) ;
#1921=CYLINDRICAL_SURFACE ( 'NONE', #4484, 15.99999999999998934 ) ;
#1924=DIRECTION ( 'NONE',  ( -1.000000000000000000, -0.000000000000000000, -7.663350976776343357E-46 ) ) ;
#1926=VERTEX_POINT ( 'NONE', #1496 ) ;
#1927=EDGE_CURVE ( 'NONE', #238, #6147, #3860, .T. ) ;
#1930=CARTESIAN_POINT ( 'NONE',  ( 21.50000000000000000, -99.90626354475340065, 72.90626354475362803 ) ) ;
#1931=CARTESIAN_POINT ( 'NONE',  ( 27.24145449743711112, -216.4945693450225974, 77.45959972289220730 ) ) ;
#1935=VECTOR ( 'NONE', #4062, 1000.000000000000114 ) ;
#1937=EDGE_CURVE ( 'NONE', #3401, #1241, #7456, .T. ) ;
#1939=CYLINDRICAL_SURFACE ( 'NONE', #3287, 7.999999999999986677 ) ;
#1941=CARTESIAN_POINT ( 'NONE',  ( 21.50000000000000000, -39.68629150101521219, 16.00000000000001421 ) ) ;
#1944=CARTESIAN_POINT ( 'NONE',  ( 21.50000000000000000, -60.68629150101523351, -11.31370849898472031 ) ) ;
#1947=EDGE_CURVE ( 'NONE', #3211, #5002, #4646, .T. ) ;
#1956=LINE ( 'NONE', #1994, #5441 ) ;
#1958=ORIENTED_EDGE ( 'NONE', *, *, #1123, .T. ) ;
#1962=CARTESIAN_POINT ( 'NONE',  ( -16.49999999999996447, 0.000000000000000000, 0.000000000000000000 ) ) ;
#1970=EDGE_LOOP ( 'NONE', ( #3272, #2704, #828, #807 ) ) ;
#1973=ORIENTED_EDGE ( 'NONE', *, *, #4742, .F. ) ;
#1974=DIRECTION ( 'NONE',  ( -1.000000000000000000, 0.000000000000000000, -7.663350976776343357E-46 ) ) ;
#1975=EDGE_CURVE ( 'NONE', #3162, #6147, #3043, .T. ) ;
#1982=CARTESIAN_POINT ( 'NONE',  ( -16.50000000000000711, -214.0630240738404382, 94.50428307177961074 ) ) ;
#1986=DIRECTION ( 'NONE',  ( -1.000000000000000000, 1.294224922628222493E-31, -1.078147950931789264E-16 ) ) ;
#1994=CARTESIAN_POINT ( 'NONE',  ( -13.64230087749234599, 16.00000000000004263, 38.63670350735201708 ) ) ;
#1995=( NAMED_UNIT ( * ) SI_UNIT ( $, .STERADIAN. ) SOLID_ANGLE_UNIT ( ) );
#2002=CARTESIAN_POINT ( 'NONE',  ( 27.03121585365657609, -225.8512969706634124, 79.74927943323393720 ) ) ;
#2004=DIRECTION ( 'NONE',  ( 1.000000000000000000, 0.000000000000000000, 7.663350976776343357E-46 ) ) ;
#2005=DIRECTION ( 'NONE',  ( -1.000000000000000000, 1.294224922628222493E-31, -1.078147950931789757E-16 ) ) ;
#2007=EDGE_CURVE ( 'NONE', #4921, #6198, #6353, .T. ) ;
#2009=CYLINDRICAL_SURFACE ( 'NONE', #2551, 7.999999999999986677 ) ;
#2052=ADVANCED_FACE ( 'NONE', ( #6504 ), #6389, .F. ) ;
#2054=FACE_OUTER_BOUND ( 'NONE', #3481, .T. ) ;
#2055=CARTESIAN_POINT ( 'NONE',  ( 10.25168462842736261, -218.0630240738404950, 95.20959099461346398 ) ) ;
#2056=VERTEX_POINT ( 'NONE', #5772 ) ;
#2067=B_SPLINE_CURVE_WITH_KNOTS ( 'NONE', 3,
 ( #4652, #6215, #3298, #5640, #3376, #2749 ),
 .UNSPECIFIED., .F., .F.,
 ( 4, 2, 4 ),
 ( 0.000000000000000000, 0.002568044547241824134, 0.005136089094483648268 ),
 .UNSPECIFIED. ) ;
#2069=VERTEX_POINT ( 'NONE', #2421 ) ;
#2076=ORIENTED_EDGE ( 'NONE', *, *, #5509, .F. ) ;
#2079=EDGE_LOOP ( 'NONE', ( #5041, #1021, #372, #440 ) ) ;
#2081=DIRECTION ( 'NONE',  ( -1.000000000000000000, 0.000000000000000000, -7.663350976776343357E-46 ) ) ;
#2082=ORIENTED_EDGE ( 'NONE', *, *, #1690, .F. ) ;
#2085=DIRECTION ( 'NONE',  ( 1.000000000000000000, 0.000000000000000000, 7.663350976776343357E-46 ) ) ;
#2086=CARTESIAN_POINT ( 'NONE',  ( -14.65391489814400572, -111.4855484589742360, 39.48554845897440657 ) ) ;
#2088=ORIENTED_EDGE ( 'NONE', *, *, #3608, .F. ) ;
#2104=ORIENTED_EDGE ( 'NONE', *, *, #3061, .T. ) ;
#2105=CARTESIAN_POINT ( 'NONE',  ( -10.49999999999997513, -39.68629150101520509, 23.99999999999999289 ) ) ;
#2107=LINE ( 'NONE', #339, #6072 ) ;
#2114=EDGE_CURVE ( 'NONE', #551, #3791, #688, .T. ) ;
#2115=DIRECTION ( 'NONE',  ( 1.000000000000000000, 0.000000000000000000, 7.663350976776343357E-46 ) ) ;
#2120=EDGE_CURVE ( 'NONE', #6255, #2955, #5426, .T. ) ;
#2164=LINE ( 'NONE', #4672, #7051 ) ;
#2171=AXIS2_PLACEMENT_3D ( 'NONE', #4656, #1755, #1178 ) ;
#2172=VERTEX_POINT ( 'NONE', #1840 ) ;
#2184=ORIENTED_EDGE ( 'NONE', *, *, #1598, .T. ) ;
#2190=FACE_OUTER_BOUND ( 'NONE', #1539, .T. ) ;
#2197=( BOUNDED_CURVE ( )  B_SPLINE_CURVE ( 3, ( #4396, #5511, #6697, #4428 ),
 .UNSPECIFIED., .F., .T. ) 
 B_SPLINE_CURVE_WITH_KNOTS ( ( 4, 4 ),
 ( 4.712388980384690562, 6.283185307179586232 ),
 .UNSPECIFIED. ) 
 CURVE ( )  GEOMETRIC_REPRESENTATION_ITEM ( )  RATIONAL_B_SPLINE_CURVE ( ( 1.000000000000000000, 0.8047378541243652705, 0.8047378541243652705, 1.000000000000000000 ) ) 
 REPRESENTATION_ITEM ( '' )  );
#2217=CARTESIAN_POINT ( 'NONE',  ( -16.49999999999999289, -120.9522879036832848, 45.92078884797942351 ) ) ;
#2219=CARTESIAN_POINT ( 'NONE',  ( 15.12446775957286604, -223.0630240738405234, 95.04560220544016147 ) ) ;
#2242=ORIENTED_EDGE ( 'NONE', *, *, #1143, .F. ) ;
#2245=DIRECTION ( 'NONE',  ( -1.000000000000000000, 0.000000000000000000, -7.663350976776343357E-46 ) ) ;
#2246=CARTESIAN_POINT ( 'NONE',  ( 17.70193531918452123, -214.7694783647498866, 94.62885002390537181 ) ) ;
#2253=ORIENTED_EDGE ( 'NONE', *, *, #875, .T. ) ;
#2254=ORIENTED_EDGE ( 'NONE', *, *, #6378, .T. ) ;
#2255=DIRECTION ( 'NONE',  ( 2.627434620609032786E-46, -0.9659258262890683122, 0.2588190451025207950 ) ) ;
#2261=EDGE_CURVE ( 'NONE', #1241, #6856, #6876, .T. ) ;
#2270=VECTOR ( 'NONE', #1194, 1000.000000000000000 ) ;
#2279=VERTEX_POINT ( 'NONE', #910 ) ;
#2282=VECTOR ( 'NONE', #6535, 1000.000000000000000 ) ;
#2287=CARTESIAN_POINT ( 'NONE',  ( 10.50256896896191527, -223.7273137069649067, 96.20835808348054741 ) ) ;
#2295=CARTESIAN_POINT ( 'NONE',  ( -19.15685424949237969, 16.00000000000004263, 36.65685424949246851 ) ) ;
#2296=DIRECTION ( 'NONE',  ( 0.7071067811865514585, 0.000000000000000000, -0.7071067811865435759 ) ) ;
#2299=CARTESIAN_POINT ( 'NONE',  ( 20.08074261902346791, -218.0630240738405519, 89.32155595708078977 ) ) ;
#2300=CARTESIAN_POINT ( 'NONE',  ( 14.39358511678551089, -223.0630240738404098, 74.09254973739808747 ) ) ;
#2307=ADVANCED_FACE ( 'NONE', ( #1519, #2647, #989 ), #1450, .F. ) ;
#2308=DIRECTION ( 'NONE',  ( -7.006492321624086910E-46, 1.221245327087672392E-15, -1.000000000000000000 ) ) ;
#2312=CARTESIAN_POINT ( 'NONE',  ( 21.50000000000000000, -49.37258300203045280, -6.000000000000027534 ) ) ;
#2320=CARTESIAN_POINT ( 'NONE',  ( 10.25562355766779277, -218.1519544391846921, 95.22527181742790958 ) ) ;
#2325=ORIENTED_EDGE ( 'NONE', *, *, #7457, .F. ) ;
#2341=ADVANCED_FACE ( 'NONE', ( #5614 ), #952, .T. ) ;
#2345=CARTESIAN_POINT ( 'NONE',  ( 21.50000000000000000, 0.000000000000000000, 0.000000000000000000 ) ) ;
#2348=CARTESIAN_POINT ( 'NONE',  ( -13.35769912250762559, -110.3978942797115508, 38.39789427971171420 ) ) ;
#2349=DIRECTION ( 'NONE',  ( 7.663350976776343357E-46, 0.000000000000000000, -1.000000000000000000 ) ) ;
#2356=CARTESIAN_POINT ( 'NONE',  ( 27.25616595088856542, -213.3481074634626680, 88.53882300612518463 ) ) ;
#2369=CARTESIAN_POINT ( 'NONE',  ( 19.22480372278612037, -223.0630240738405234, 91.70218713096633678 ) ) ;
#2372=LINE ( 'NONE', #3609, #7459 ) ;
#2374=DIRECTION ( 'NONE',  ( -3.379803290564628095E-16, -1.221245327087672392E-15, 1.000000000000000000 ) ) ;
#2377=LINE ( 'NONE', #7074, #370 ) ;
#2378=ORIENTED_EDGE ( 'NONE', *, *, #2120, .T. ) ;
#2385=CARTESIAN_POINT ( 'NONE',  ( -16.49999999999996447, -60.68629150101523351, -11.31370849898472031 ) ) ;
#2390=EDGE_LOOP ( 'NONE', ( #3341, #2254, #6217, #261 ) ) ;
#2392=CARTESIAN_POINT ( 'NONE',  ( 10.21539232130207964, -217.2436419687049067, 95.06511182196837240 ) ) ;
#2402=VECTOR ( 'NONE', #2081, 1000.000000000000000 ) ;
#2408=CIRCLE ( 'NONE', #4809, 15.99999999999997335 ) ;
#2411=AXIS2_PLACEMENT_3D ( 'NONE', #5647, #338, #2756 ) ;
#2421=CARTESIAN_POINT ( 'NONE',  ( -13.35769912250762914, -65.39789427971170710, 38.39789427971182789 ) ) ;
#2427=FACE_OUTER_BOUND ( 'NONE', #2390, .T. ) ;
#2433=CARTESIAN_POINT ( 'NONE',  ( 17.67236366837565953, -217.7372475398859137, 71.85424062197721184 ) ) ;
#2434=EDGE_LOOP ( 'NONE', ( #274, #5135, #5652, #2679 ) ) ;
#2437=LINE ( 'NONE', #1240, #4343 ) ;
#2440=EDGE_CURVE ( 'NONE', #1259, #5789, #2776, .T. ) ;
#2454=APPLICATION_CONTEXT ( 'automotive_design' ) ;
#2458=DIRECTION ( 'NONE',  ( -1.000000000000000000, 0.000000000000000000, -7.663350976776343357E-46 ) ) ;
#2464=VERTEX_POINT ( 'NONE', #6990 ) ;
#2466=CARTESIAN_POINT ( 'NONE',  ( 17.77671317003690632, -224.6695236240147722, 73.71173840043843484 ) ) ;
#2471=FACE_OUTER_BOUND ( 'NONE', #6515, .T. ) ;
#2482=VECTOR ( 'NONE', #7377, 999.9999999999998863 ) ;
#2490=( BOUNDED_CURVE ( )  B_SPLINE_CURVE ( 3, ( #142, #2942, #19, #1211 ),
 .UNSPECIFIED., .F., .T. ) 
 B_SPLINE_CURVE_WITH_KNOTS ( ( 4, 4 ),
 ( 4.712388980384686121, 5.497787143782135288 ),
 .UNSPECIFIED. ) 
 CURVE ( )  GEOMETRIC_REPRESENTATION_ITEM ( )  RATIONAL_B_SPLINE_CURVE ( ( 1.000000000000000000, 0.9492530216741910110, 0.9492530216741910110, 1.000000000000000000 ) ) 
 REPRESENTATION_ITEM ( '' )  );
#2491=EDGE_LOOP ( 'NONE', ( #3567, #4269 ) ) ;
#2494=CARTESIAN_POINT ( 'NONE',  ( 21.50000000000000000, -45.34314575050758123, 18.34314575050765939 ) ) ;
#2503=CIRCLE ( 'NONE', #5328, 8.000000000000007105 ) ;
#2504=DIRECTION ( 'NONE',  ( -3.503246160812042677E-46, -0.7071067811865485719, -0.7071067811865464625 ) ) ;
#2505=CARTESIAN_POINT ( 'NONE',  ( 27.12317295347672541, -221.7587214059826692, 78.74778750054862542 ) ) ;
#2524=AXIS2_PLACEMENT_3D ( 'NONE', #6431, #2349, #7041 ) ;
#2531=DIRECTION ( 'NONE',  ( 0.000000000000000000, 0.000000000000000000, 1.000000000000000000 ) ) ;
#2535=ADVANCED_FACE ( 'NONE', ( #6641 ), #4225, .F. ) ;
#2540=VECTOR ( 'NONE', #6220, 1000.000000000000114 ) ;
#2547=CARTESIAN_POINT ( 'NONE',  ( 10.33013951010423170, -224.6695236240153122, 73.71173840043077519 ) ) ;
#2551=AXIS2_PLACEMENT_3D ( 'NONE', #4323, #3168, #6665 ) ;
#2563=ORIENTED_EDGE ( 'NONE', *, *, #4005, .F. ) ;
#2575=VERTEX_POINT ( 'NONE', #1982 ) ;
#2584=DIRECTION ( 'NONE',  ( -1.000000000000000000, 0.000000000000000000, -7.663350976776343357E-46 ) ) ;
#2586=CARTESIAN_POINT ( 'NONE',  ( -10.49999999999996803, 0.000000000000000000, 0.000000000000000000 ) ) ;
#2587=ORIENTED_EDGE ( 'NONE', *, *, #5314, .T. ) ;
#2590=DIRECTION ( 'NONE',  ( -1.000000000000000000, 0.000000000000000000, -7.663350976776343357E-46 ) ) ;
#2597=CYLINDRICAL_SURFACE ( 'NONE', #4621, 15.99999999999999645 ) ;
#2605=EDGE_CURVE ( 'NONE', #1241, #3224, #183, .T. ) ;
#2629=LINE ( 'NONE', #6859, #1351 ) ;
#2638=CARTESIAN_POINT ( 'NONE',  ( 21.50000000000000000, 0.000000000000000000, 0.000000000000000000 ) ) ;
#2645=ORIENTED_EDGE ( 'NONE', *, *, #1927, .T. ) ;
#2647=FACE_BOUND ( 'NONE', #6328, .T. ) ;
#2654=CARTESIAN_POINT ( 'NONE',  ( -10.49999999999996803, -49.37258300203045280, 5.999999999999972466 ) ) ;
#2658=AXIS2_PLACEMENT_3D ( 'NONE', #1944, #7067, #3068 ) ;
#2659=B_SPLINE_CURVE_WITH_KNOTS ( 'NONE', 3,
 ( #2853, #6364, #6975, #1699 ),
 .UNSPECIFIED., .F., .F.,
 ( 4, 4 ),
 ( 0.000000000000000000, 1.000000000000000000 ),
 .UNSPECIFIED. ) ;
#2661=CARTESIAN_POINT ( 'NONE',  ( -13.64230087749234599, -110.6367035073516689, 38.63670350735182524 ) ) ;
#2666=DIRECTION ( 'NONE',  ( -7.006492321624086910E-46, 1.221245327087672392E-15, -1.000000000000000000 ) ) ;
#2675=CARTESIAN_POINT ( 'NONE',  ( -16.50000000000001066, -216.4061698243480691, 94.91744288732648727 ) ) ;
#2679=ORIENTED_EDGE ( 'NONE', *, *, #171, .F. ) ;
#2688=ORIENTED_EDGE ( 'NONE', *, *, #4139, .F. ) ;
#2690=ORIENTED_EDGE ( 'NONE', *, *, #1361, .T. ) ;
#2701=DIRECTION ( 'NONE',  ( 0.000000000000000000, 1.000000000000000000, 1.734723475976805517E-15 ) ) ;
#2702=AXIS2_PLACEMENT_3D ( 'NONE', #7294, #5495, #1478 ) ;
#2704=ORIENTED_EDGE ( 'NONE', *, *, #2007, .T. ) ;
#2720=DIRECTION ( 'NONE',  ( 0.000000000000000000, 0.000000000000000000, -1.000000000000000000 ) ) ;
#2739=EDGE_CURVE ( 'NONE', #5684, #1669, #852, .T. ) ;
#2745=DIRECTION ( 'NONE',  ( 1.000000000000000000, 0.000000000000000000, 7.663350976776343357E-46 ) ) ;
#2749=CARTESIAN_POINT ( 'NONE',  ( -16.49999999999998934, -117.9145199278634522, 44.76505905230362714 ) ) ;
#2753=ORIENTED_EDGE ( 'NONE', *, *, #4174, .F. ) ;
#2756=DIRECTION ( 'NONE',  ( 0.000000000000000000, 0.000000000000000000, 1.000000000000000000 ) ) ;
#2758=CARTESIAN_POINT ( 'NONE',  ( 35.75983027283935201, -69.18339347973481779, -2.816606520265163560 ) ) ;
#2762=CARTESIAN_POINT ( 'NONE',  ( -16.50000000000000000, -99.90626354475340065, 72.90626354475362803 ) ) ;
#2771=CARTESIAN_POINT ( 'NONE',  ( -16.49999999999997513, -104.8363803175325160, 32.83638031753267938 ) ) ;
#2773=ORIENTED_EDGE ( 'NONE', *, *, #5931, .F. ) ;
#2774=ADVANCED_FACE ( 'NONE', ( #6599 ), #3714, .F. ) ;
#2776=CIRCLE ( 'NONE', #2171, 15.99999999999998934 ) ;
#2792=CARTESIAN_POINT ( 'NONE',  ( -10.49999999999997513, -6.938893903907228378E-15, 15.99999999999998579 ) ) ;
#2799=CARTESIAN_POINT ( 'NONE',  ( -21.50000000000000000, -215.0630240738404950, 94.68061005248806339 ) ) ;
#2809=VERTEX_POINT ( 'NONE', #3288 ) ;
#2810=CARTESIAN_POINT ( 'NONE',  ( -16.49999999999996447, -49.37258300203045280, -2.775557561562891351E-14 ) ) ;
#2814=CARTESIAN_POINT ( 'NONE',  ( 27.08493024494318746, -221.0431231857559737, 90.06937369499782164 ) ) ;
#2829=CARTESIAN_POINT ( 'NONE',  ( 18.05944481925498479, -223.0630240738404382, 76.51671422530451139 ) ) ;
#2841=EDGE_CURVE ( 'NONE', #5002, #6433, #3864, .T. ) ;
#2842=VECTOR ( 'NONE', #7154, 1000.000000000000000 ) ;
#2843=EDGE_LOOP ( 'NONE', ( #1425, #5633, #6457, #7046, #4589, #2645, #6226, #1713 ) ) ;
#2851=VECTOR ( 'NONE', #4347, 1000.000000000000000 ) ;
#2853=CARTESIAN_POINT ( 'NONE',  ( 10.03180245857092423, -218.0630240738404382, 71.94153218116483117 ) ) ;
#2854=CARTESIAN_POINT ( 'NONE',  ( 27.03121585365657609, -223.4569485227348480, 90.54948733812101125 ) ) ;
#2873=EDGE_CURVE ( 'NONE', #3791, #1259, #36, .T. ) ;
#2876=FACE_OUTER_BOUND ( 'NONE', #5262, .T. ) ;
#2894=CARTESIAN_POINT ( 'NONE',  ( 17.80066350777958917, -221.4565245236572935, 95.80795668296067902 ) ) ;
#2901=ORIENTED_EDGE ( 'NONE', *, *, #1975, .T. ) ;
#2902=CARTESIAN_POINT ( 'NONE',  ( -19.15685424949238680, -108.6568542494921701, 36.65685424949233351 ) ) ;
#2905=CARTESIAN_POINT ( 'NONE',  ( 20.88432520271932447, -218.0630240738405519, 79.82767783018041996 ) ) ;
#2913=CARTESIAN_POINT ( 'NONE',  ( 10.47314606205195631, -223.0630240738404666, 96.09122589815579829 ) ) ;
#2920=DIRECTION ( 'NONE',  ( 1.000000000000000000, 0.000000000000000000, 7.663350976776343357E-46 ) ) ;
#2921=LINE ( 'NONE', #3044, #6688 ) ;
#2927=ORIENTED_EDGE ( 'NONE', *, *, #37, .F. ) ;
#2929=CARTESIAN_POINT ( 'NONE',  ( 27.24145449743711112, -214.0092129552772633, 88.67031792470811524 ) ) ;
#2933=CARTESIAN_POINT ( 'NONE',  ( -10.49999999999996803, -49.37258300203045280, -2.775557561562891351E-14 ) ) ;
#2941=CARTESIAN_POINT ( 'NONE',  ( 19.96154802696617736, -223.0630240738404666, 90.65370741215697592 ) ) ;
#2942=CARTESIAN_POINT ( 'NONE',  ( -16.49999999999996447, -59.83638031753262965, 32.83638031753273623 ) ) ;
#2949=CARTESIAN_POINT ( 'NONE',  ( -18.84314575050759188, -63.34314575050751017, 36.34314575050759544 ) ) ;
#2955=VERTEX_POINT ( 'NONE', #5649 ) ;
#2962=B_SPLINE_CURVE_WITH_KNOTS ( 'NONE', 3,
 ( #3420, #1094, #1173, #3456, #479, #1133, #2300, #7482, #1792, #5797, #5759, #6951, #2829, #1058, #3989, #5218, #1627, #6453, #5905, #4568, #18, #594, #1751, #5291, #2941, #2369, #6376, #4032, #4146, #6489, #4686, #1210, #3565, #2219, #4725, #6907, #6985, #518 ),
 .UNSPECIFIED., .F., .F.,
 ( 4, 1, 1, 2, 2, 1, 1, 2, 2, 2, 2, 1, 1, 2, 2, 1, 1, 2, 2, 1, 1, 2, 2, 4 ),
 ( 0.000000000000000000, 0.06249999999999945877, 0.09374999999999929223, 0.1093749999999992228, 0.1249999999999991396, 0.1874999999999995837, 0.2187499999999996392, 0.2343749999999995282, 0.2499999999999994449, 0.3749999999999973910, 0.4999999999999953926, 0.5624999999999948930, 0.5937499999999941158, 0.6093749999999936717, 0.6249999999999933387, 0.6874999999999940048, 0.7187499999999943379, 0.7343749999999946709, 0.7499999999999948930, 0.8124999999999957812, 0.8437499999999958922, 0.8593749999999960032, 0.8749999999999961142, 1.000000000000000000 ),
 .UNSPECIFIED. ) ;
#2970=CARTESIAN_POINT ( 'NONE',  ( 17.81252276423129999, -222.2597742987536265, 95.94959129056174163 ) ) ;
#2978=AXIS2_PLACEMENT_3D ( 'NONE', #5231, #7566, #7458 ) ;
#2980=CARTESIAN_POINT ( 'NONE',  ( 17.59106180226908478, -218.0630240738404950, 74.83367537032552264 ) ) ;
#2983=EDGE_CURVE ( 'NONE', #6591, #628, #1956, .T. ) ;
#2985=EDGE_LOOP ( 'NONE', ( #6006, #2082, #7148, #4261, #5998 ) ) ;
#3002=EDGE_CURVE ( 'NONE', #2575, #687, #5576, .T. ) ;
#3005=EDGE_CURVE ( 'NONE', #5964, #578, #7266, .T. ) ;
#3006=ORIENTED_EDGE ( 'NONE', *, *, #1153, .T. ) ;
#3010=EDGE_LOOP ( 'NONE', ( #6344, #3292, #4287, #926 ) ) ;
#3012=CARTESIAN_POINT ( 'NONE',  ( 10.40199052334513041, -226.2606222968796601, 74.13807200490302307 ) ) ;
#3027=CARTESIAN_POINT ( 'NONE',  ( 15.61587190384303980, -218.0630240738405519, 73.42250040783586940 ) ) ;
#3029=UNCERTAINTY_MEASURE_WITH_UNIT (LENGTH_MEASURE( 1.000000000000000082E-05 ), #1374, 'distance_accuracy_value', 'NONE');
#3037=( BOUNDED_CURVE ( )  B_SPLINE_CURVE ( 3, ( #5153, #3924, #6422, #1639 ),
 .UNSPECIFIED., .F., .T. ) 
 B_SPLINE_CURVE_WITH_KNOTS ( ( 4, 4 ),
 ( 1.570796326794896558, 2.443460952792054552 ),
 .UNSPECIFIED. ) 
 CURVE ( )  GEOMETRIC_REPRESENTATION_ITEM ( )  RATIONAL_B_SPLINE_CURVE ( ( 1.000000000000000000, 0.9375385246911008830, 0.9375385246911008830, 1.000000000000000000 ) ) 
 REPRESENTATION_ITEM ( '' )  );
#3040=ORIENTED_EDGE ( 'NONE', *, *, #5413, .T. ) ;
#3041=EDGE_CURVE ( 'NONE', #4710, #3465, #4042, .T. ) ;
#3043=CIRCLE ( 'NONE', #4777, 8.000000000000007105 ) ;
#3044=CARTESIAN_POINT ( 'NONE',  ( 26.37580566599013920, -63.12419433401035462, -8.875805665989638271 ) ) ;
#3055=CARTESIAN_POINT ( 'NONE',  ( 27.19709702122541017, -218.4687108041559895, 77.94269080187306997 ) ) ;
#3058=DIRECTION ( 'NONE',  ( -4.336808689942025132E-16, 3.989863994746663259E-14, 1.000000000000000000 ) ) ;
#3061=EDGE_CURVE ( 'NONE', #3465, #6591, #3037, .T. ) ;
#3064=( NAMED_UNIT ( * ) PLANE_ANGLE_UNIT ( ) SI_UNIT ( $, .RADIAN. ) );
#3068=DIRECTION ( 'NONE',  ( 2.627434620609032786E-46, -0.7071067811865464625, 0.7071067811865485719 ) ) ;
#3069=ADVANCED_FACE ( 'NONE', ( #2876 ), #3391, .F. ) ;
#3084=EDGE_CURVE ( 'NONE', #6198, #1926, #7271, .T. ) ;
#3085=ADVANCED_FACE ( 'NONE', ( #2190 ), #6385, .F. ) ;
#3086=ORIENTED_EDGE ( 'NONE', *, *, #7167, .F. ) ;
#3089=CARTESIAN_POINT ( 'NONE',  ( 9.987668098222851398, -217.0856944719845387, 71.67965750360849597 ) ) ;
#3097=VECTOR ( 'NONE', #3207, 1000.000000000000000 ) ;
#3105=CARTESIAN_POINT ( 'NONE',  ( -21.50000000000000000, -114.3401965514817817, 42.31370849898471675 ) ) ;
#3121=CARTESIAN_POINT ( 'NONE',  ( 27.10306686690893940, -222.6535482193571909, 78.96676008164924099 ) ) ;
#3122=EDGE_LOOP ( 'NONE', ( #2927, #6139, #4922, #4547 ) ) ;
#3128=CARTESIAN_POINT ( 'NONE',  ( -13.49999999999999822, -223.0630240738404382, 73.28127814332047762 ) ) ;
#3130=EDGE_CURVE ( 'NONE', #3448, #1532, #4829, .T. ) ;
#3131=AXIS2_PLACEMENT_3D ( 'NONE', #6409, #4797, #2296 ) ;
#3132=DIRECTION ( 'NONE',  ( -1.000000000000000000, 1.294224922628222493E-31, -1.078147950931789264E-16 ) ) ;
#3137=CARTESIAN_POINT ( 'NONE',  ( -16.50000000000000000, -104.1739323729103717, 75.12787131935894536 ) ) ;
#3145=DIRECTION ( 'NONE',  ( 0.000000000000000000, 0.000000000000000000, -1.000000000000000000 ) ) ;
#3153=VECTOR ( 'NONE', #4849, 1000.000000000000000 ) ;
#3154=CARTESIAN_POINT ( 'NONE',  ( -16.49999999999996447, -60.68629150101523351, -11.31370849898472031 ) ) ;
#3157=ORIENTED_EDGE ( 'NONE', *, *, #3333, .F. ) ;
#3162=VERTEX_POINT ( 'NONE', #3431 ) ;
#3165=DIRECTION ( 'NONE',  ( -1.000000000000000000, 0.000000000000000000, -7.663350976776343357E-46 ) ) ;
#3168=DIRECTION ( 'NONE',  ( 0.000000000000000000, -1.000000000000000000, -1.221245327087672392E-15 ) ) ;
#3171=CARTESIAN_POINT ( 'NONE',  ( 21.50000000000000000, -39.68629150101520509, 23.99999999999999289 ) ) ;
#3176=B_SPLINE_CURVE_WITH_KNOTS ( 'NONE', 3,
 ( #3105, #3259, #752, #5454 ),
 .UNSPECIFIED., .F., .F.,
 ( 4, 4 ),
 ( 5.887846720064191696E-17, 0.0007743866022177889373 ),
 .UNSPECIFIED. ) ;
#3179=FACE_OUTER_BOUND ( 'NONE', #22, .T. ) ;
#3202=CYLINDRICAL_SURFACE ( 'NONE', #705, 5.999999999999999112 ) ;
#3206=EDGE_LOOP ( 'NONE', ( #5928, #4434, #1817, #462, #3684, #2242, #5628, #341 ) ) ;
#3207=DIRECTION ( 'NONE',  ( -1.000000000000000000, 0.000000000000000000, -7.663350976776343357E-46 ) ) ;
#3211=VERTEX_POINT ( 'NONE', #6463 ) ;
#3215=VECTOR ( 'NONE', #717, 1000.000000000000000 ) ;
#3224=VERTEX_POINT ( 'NONE', #4228 ) ;
#3226=EDGE_CURVE ( 'NONE', #1532, #3586, #2377, .T. ) ;
#3242=CIRCLE ( 'NONE', #6180, 15.99999999999998934 ) ;
#3243=CARTESIAN_POINT ( 'NONE',  ( -21.49999999999999645, -219.7493155748557285, 72.39337262706533238 ) ) ;
#3259=CARTESIAN_POINT ( 'NONE',  ( -21.49999999999999289, -114.1489496936987393, 42.14012972382754896 ) ) ;
#3266=VECTOR ( 'NONE', #1130, 1000.000000000000000 ) ;
#3272=ORIENTED_EDGE ( 'NONE', *, *, #3403, .F. ) ;
#3275=LINE ( 'NONE', #3853, #1030 ) ;
#3287=AXIS2_PLACEMENT_3D ( 'NONE', #3525, #630, #15 ) ;
#3288=CARTESIAN_POINT ( 'NONE',  ( -12.50000000000000355, -218.0630240738404382, 71.94153218116483117 ) ) ;
#3292=ORIENTED_EDGE ( 'NONE', *, *, #2841, .T. ) ;
#3293=ADVANCED_FACE ( 'NONE', ( #4340 ), #5530, .F. ) ;
#3298=CARTESIAN_POINT ( 'NONE',  ( -16.30128210308657088, -115.0146905589846256, 42.92178193144403764 ) ) ;
#3303=CARTESIAN_POINT ( 'NONE',  ( -21.50000000000000000, -104.1739323729103432, 75.12787131935894536 ) ) ;
#3310=CARTESIAN_POINT ( 'NONE',  ( -10.49999999999997513, -39.68629150101519087, 15.99999999999998579 ) ) ;
#3319=CARTESIAN_POINT ( 'NONE',  ( -21.50000000000000000, -120.9522879036832848, 45.92078884797942351 ) ) ;
#3329=DIRECTION ( 'NONE',  ( 0.000000000000000000, -1.000000000000000000, -1.221245327087672392E-15 ) ) ;
#3330=LINE ( 'NONE', #443, #5715 ) ;
#3333=EDGE_CURVE ( 'NONE', #6856, #578, #6025, .T. ) ;
#3335=CARTESIAN_POINT ( 'NONE',  ( -19.15685424949238325, -63.65685424949226245, 36.65685424949236193 ) ) ;
#3341=ORIENTED_EDGE ( 'NONE', *, *, #6156, .T. ) ;
#3367=EDGE_CURVE ( 'NONE', #3586, #5789, #1447, .T. ) ;
#3369=CARTESIAN_POINT ( 'NONE',  ( -13.64230087749234599, 16.00000000000004263, 38.63670350735201708 ) ) ;
#3376=CARTESIAN_POINT ( 'NONE',  ( -16.49999999999998934, -117.1391065123254407, 44.37576177830231217 ) ) ;
#3384=CARTESIAN_POINT ( 'NONE',  ( -16.49999999999996447, -49.37258300203045280, -6.000000000000029310 ) ) ;
#3391=PLANE ( 'NONE',  #2978 ) ;
#3393=PRODUCT_DEFINITION_FORMATION_WITH_SPECIFIED_SOURCE ( 'ANY', '', #6529, .NOT_KNOWN. ) ;
#3397=ORIENTED_EDGE ( 'NONE', *, *, #6685, .T. ) ;
#3398=CARTESIAN_POINT ( 'NONE',  ( -17.32280336819469468, -106.8228033681944993, 34.82280336819463429 ) ) ;
#3400=CARTESIAN_POINT ( 'NONE',  ( -10.49999999999997691, -45.34314575050758123, 18.34314575050765939 ) ) ;
#3401=VERTEX_POINT ( 'NONE', #5456 ) ;
#3403=EDGE_CURVE ( 'NONE', #4921, #877, #1107, .T. ) ;
#3420=CARTESIAN_POINT ( 'NONE',  ( 10.25759302228802738, -223.0630240738404382, 73.28127814332047762 ) ) ;
#3424=AXIS2_PLACEMENT_3D ( 'NONE', #2345, #81, #1762 ) ;
#3426=ORIENTED_EDGE ( 'NONE', *, *, #1670, .F. ) ;
#3431=CARTESIAN_POINT ( 'NONE',  ( -21.50000000000000000, -99.90626354475340065, 72.90626354475362803 ) ) ;
#3436=EDGE_LOOP ( 'NONE', ( #1384, #4582, #3426, #7042 ) ) ;
#3437=CARTESIAN_POINT ( 'NONE',  ( -16.49999999999996447, -102.6862915010150203, 30.68629150101515179 ) ) ;
#3442=CARTESIAN_POINT ( 'NONE',  ( 17.76462208873361348, -219.0153713307822727, 95.37751551101582947 ) ) ;
#3448=VERTEX_POINT ( 'NONE', #2792 ) ;
#3455=CARTESIAN_POINT ( 'NONE',  ( 20.57205124765284765, -218.0630240738404950, 88.30031236728251542 ) ) ;
#3456=CARTESIAN_POINT ( 'NONE',  ( 13.34421828821804112, -223.0630240738404950, 73.71416242504422200 ) ) ;
#3462=CARTESIAN_POINT ( 'NONE',  ( -13.49999999999999822, -223.0630240738404666, 96.09122589815579829 ) ) ;
#3465=VERTEX_POINT ( 'NONE', #4033 ) ;
#3469=CARTESIAN_POINT ( 'NONE',  ( -18.84314575050759188, -108.3431457505073752, 36.34314575050756702 ) ) ;
#3476=CARTESIAN_POINT ( 'NONE',  ( 27.12218822116579631, -219.3688186872617223, 89.73635190582673715 ) ) ;
#3481=EDGE_LOOP ( 'NONE', ( #1051, #7570, #384, #955 ) ) ;
#3487=CARTESIAN_POINT ( 'NONE',  ( 15.34038085515988392, -218.0630240738405519, 93.99974598701426487 ) ) ;
#3518=CARTESIAN_POINT ( 'NONE',  ( 17.77671317003690632, -219.8343230396697550, 95.52191879319198620 ) ) ;
#3521=CARTESIAN_POINT ( 'NONE',  ( -21.50000000000000000, -114.3401965514817817, 42.31370849898471675 ) ) ;
#3523=EDGE_CURVE ( 'NONE', #2172, #2464, #2067, .T. ) ;
#3525=CARTESIAN_POINT ( 'NONE',  ( -8.500000000000003553, 16.00000000000003908, 44.76505905230376925 ) ) ;
#3540=AXIS2_PLACEMENT_3D ( 'NONE', #4028, #4098, #2255 ) ;
#3542=ORIENTED_EDGE ( 'NONE', *, *, #3673, .T. ) ;
#3560=VERTEX_POINT ( 'NONE', #1059 ) ;
#3564=CARTESIAN_POINT ( 'NONE',  ( 20.30051329250314396, -218.0630240738406087, 78.41711159333182479 ) ) ;
#3565=CARTESIAN_POINT ( 'NONE',  ( 15.45545259347109379, -223.0630240738404950, 94.88225035920650896 ) ) ;
#3566=CARTESIAN_POINT ( 'NONE',  ( -10.49999999999996803, -49.37258300203047412, -15.99999999999998579 ) ) ;
#3567=ORIENTED_EDGE ( 'NONE', *, *, #1061, .T. ) ;
#3573=CARTESIAN_POINT ( 'NONE',  ( -11.51602904742826716, -63.85254959896234794, 36.85254959896245452 ) ) ;
#3586=VERTEX_POINT ( 'NONE', #3566 ) ;
#3595=CARTESIAN_POINT ( 'NONE',  ( 9.987668098222851398, -212.1022451272886826, 94.15854484029739524 ) ) ;
#3598=DIRECTION ( 'NONE',  ( -7.006492321624086910E-46, 1.221245327087672392E-15, -1.000000000000000000 ) ) ;
#3604=CARTESIAN_POINT ( 'NONE',  ( 20.41805204809246632, -218.0630240738405234, 88.64886852284689667 ) ) ;
#3608=EDGE_CURVE ( 'NONE', #877, #4921, #1099, .T. ) ;
#3609=CARTESIAN_POINT ( 'NONE',  ( 21.50000000000000000, -113.7796841263388501, 41.77968412633906325 ) ) ;
#3637=CARTESIAN_POINT ( 'NONE',  ( -16.50000000000000000, -214.0630240738404382, 70.86973541144034527 ) ) ;
#3640=EDGE_CURVE ( 'NONE', #7269, #2056, #6563, .T. ) ;
#3643=CYLINDRICAL_SURFACE ( 'NONE', #6323, 6.000000000000000000 ) ;
#3644=APPLICATION_CONTEXT ( 'automotive_design' ) ;
#3671=CARTESIAN_POINT ( 'NONE',  ( 10.29386626619291434, -223.8662738488881701, 73.49650827186496826 ) ) ;
#3673=EDGE_CURVE ( 'NONE', #551, #7269, #2490, .T. ) ;
#3679=ORIENTED_EDGE ( 'NONE', *, *, #7167, .T. ) ;
#3684=ORIENTED_EDGE ( 'NONE', *, *, #5076, .F. ) ;
#3685=CARTESIAN_POINT ( 'NONE',  ( -21.50000000000000000, -99.90626354475340065, 72.90626354475362803 ) ) ;
#3689=DIRECTION ( 'NONE',  ( -4.336808689942013792E-16, 0.000000000000000000, 1.000000000000000000 ) ) ;
#3692=ORIENTED_EDGE ( 'NONE', *, *, #1410, .T. ) ;
#3704=FACE_OUTER_BOUND ( 'NONE', #4105, .T. ) ;
#3711=EDGE_CURVE ( 'NONE', #105, #5964, #7008, .T. ) ;
#3714=CYLINDRICAL_SURFACE ( 'NONE', #1746, 7.999999999999986677 ) ;
#3716=CARTESIAN_POINT ( 'NONE',  ( -16.49999999999996447, -102.6862915010150203, 30.68629150101515179 ) ) ;
#3729=VERTEX_POINT ( 'NONE', #2055 ) ;
#3738=ORIENTED_EDGE ( 'NONE', *, *, #2739, .T. ) ;
#3743=CARTESIAN_POINT ( 'NONE',  ( 17.83418965632456121, -228.4878731603066910, 74.73486207509358792 ) ) ;
#3755=FACE_OUTER_BOUND ( 'NONE', #1970, .T. ) ;
#3756=AXIS2_PLACEMENT_3D ( 'NONE', #1364, #5527, #330 ) ;
#3781=CARTESIAN_POINT ( 'NONE',  ( 27.21559789597881007, -217.6453243769068706, 77.74120035865662715 ) ) ;
#3788=CARTESIAN_POINT ( 'NONE',  ( 21.50000000000000000, -104.1739323729103432, 75.12787131935894536 ) ) ;
#3791=VERTEX_POINT ( 'NONE', #3716 ) ;
#3794=DIRECTION ( 'NONE',  ( 0.000000000000000000, 0.000000000000000000, 1.000000000000000000 ) ) ;
#3798=CARTESIAN_POINT ( 'NONE',  ( 21.50000000000000000, 0.000000000000000000, 5.999999999999999112 ) ) ;
#3813=ADVANCED_FACE ( 'NONE', ( #6671 ), #1394, .F. ) ;
#3819=AXIS2_PLACEMENT_3D ( 'NONE', #5668, #2666, #2701 ) ;
#3820=( BOUNDED_CURVE ( )  B_SPLINE_CURVE ( 3, ( #2799, #4501, #4657, #3998 ),
 .UNSPECIFIED., .F., .T. ) 
 B_SPLINE_CURVE_WITH_KNOTS ( ( 4, 4 ),
 ( 1.570796326794896558, 3.141592653589793116 ),
 .UNSPECIFIED. ) 
 CURVE ( )  GEOMETRIC_REPRESENTATION_ITEM ( )  RATIONAL_B_SPLINE_CURVE ( ( 1.000000000000000000, 0.8047378541243649375, 0.8047378541243649375, 1.000000000000000000 ) ) 
 REPRESENTATION_ITEM ( '' )  );
#3838=DIRECTION ( 'NONE',  ( -1.000000000000000000, 0.000000000000000000, -7.663350976776343357E-46 ) ) ;
#3853=CARTESIAN_POINT ( 'NONE',  ( -22.93100982128538234, -73.43085575620197858, 46.43085575620212069 ) ) ;
#3860=LINE ( 'NONE', #3788, #4027 ) ;
#3864=LINE ( 'NONE', #4555, #5066 ) ;
#3877=CARTESIAN_POINT ( 'NONE',  ( -14.84314575050763096, -218.0630240738404666, 95.20959099461347819 ) ) ;
#3924=CARTESIAN_POINT ( 'NONE',  ( -16.49999999999998224, -69.36092951174981636, 42.36092951174991583 ) ) ;
#3948=LINE ( 'NONE', #362, #5230 ) ;
#3957=CARTESIAN_POINT ( 'NONE',  ( 14.52070450238005606, -218.0630240738404666, 72.88438438556153187 ) ) ;
#3962=AXIS2_PLACEMENT_3D ( 'NONE', #4003, #1105, #2720 ) ;
#3973=DIRECTION ( 'NONE',  ( -7.663350976776344912E-46, 0.000000000000000000, -1.000000000000000000 ) ) ;
#3975=ORIENTED_EDGE ( 'NONE', *, *, #3711, .T. ) ;
#3989=CARTESIAN_POINT ( 'NONE',  ( 20.03634105971836377, -223.0630240738403813, 78.93565216506947024 ) ) ;
#3998=CARTESIAN_POINT ( 'NONE',  ( -13.49999999999999822, -223.0630240738404666, 96.09122589815579829 ) ) ;
#4003=CARTESIAN_POINT ( 'NONE',  ( -16.49999999999996447, -49.37258300203045280, -2.775557561562891351E-14 ) ) ;
#4005=EDGE_CURVE ( 'NONE', #4710, #3162, #556, .T. ) ;
#4008=LINE ( 'NONE', #3310, #6574 ) ;
#4014=EDGE_CURVE ( 'NONE', #5692, #3401, #2437, .T. ) ;
#4019=FACE_OUTER_BOUND ( 'NONE', #2434, .T. ) ;
#4027=VECTOR ( 'NONE', #5553, 1000.000000000000000 ) ;
#4028=CARTESIAN_POINT ( 'NONE',  ( 21.50000000000000000, -120.9522879036832848, 45.92078884797942351 ) ) ;
#4032=CARTESIAN_POINT ( 'NONE',  ( 18.63431107999237923, -223.0630240738404666, 92.40830921507968299 ) ) ;
#4033=CARTESIAN_POINT ( 'NONE',  ( -16.49999999999998934, -71.76505905230354188, 44.76505905230365556 ) ) ;
#4042=LINE ( 'NONE', #2762, #4451 ) ;
#4062=DIRECTION ( 'NONE',  ( -0.5773502691896310601, -0.5773502691896222894, 0.5773502691896238437 ) ) ;
#4066=CARTESIAN_POINT ( 'NONE',  ( 16.72842210847736766, -218.0630240738404950, 74.10707748653940996 ) ) ;
#4069=AXIS2_PLACEMENT_3D ( 'NONE', #934, #1543, #1501 ) ;
#4074=LINE ( 'NONE', #6571, #2282 ) ;
#4085=DIRECTION ( 'NONE',  ( 0.000000000000000000, 0.000000000000000000, -1.000000000000000000 ) ) ;
#4098=DIRECTION ( 'NONE',  ( 4.379057701015054125E-46, 0.2588190451025207950, 0.9659258262890683122 ) ) ;
#4104=CARTESIAN_POINT ( 'NONE',  ( -18.84314575050759188, 16.00000000000006395, 36.34314575050770202 ) ) ;
#4105=EDGE_LOOP ( 'NONE', ( #2184, #3975, #2690, #2563, #6844, #2104, #6547, #5304, #3006, #3040, #4397, #3542 ) ) ;
#4106=AXIS2_PLACEMENT_3D ( 'NONE', #2105, #951, #5150 ) ;
#4110=CARTESIAN_POINT ( 'NONE',  ( -12.50000000000001066, -218.0630240738404950, 95.20959099461346398 ) ) ;
#4119=VECTOR ( 'NONE', #1187, 1000.000000000000000 ) ;
#4132=CARTESIAN_POINT ( 'NONE',  ( 10.29386626619291434, -219.0153713307822727, 95.37751551101595737 ) ) ;
#4139=EDGE_CURVE ( 'NONE', #3586, #6255, #3242, .T. ) ;
#4145=CARTESIAN_POINT ( 'NONE',  ( 12.13610945967080923, -218.0630240738405519, 95.09600923956017482 ) ) ;
#4146=CARTESIAN_POINT ( 'NONE',  ( 18.51125185374242932, -223.0630240738404950, 92.54436274715045840 ) ) ;
#4152=DIRECTION ( 'NONE',  ( 5.254869241218065572E-46, -0.7071067811865465735, 0.7071067811865485719 ) ) ;
#4155=PRODUCT_DEFINITION ( 'UNKNOWN', '', #3393, #21 ) ;
#4162=DIRECTION ( 'NONE',  ( -1.000000000000000000, 0.000000000000000000, -7.663350976776343357E-46 ) ) ;
#4171=CARTESIAN_POINT ( 'NONE',  ( 17.73846410710429211, -217.2436419687045657, 95.06511182196470600 ) ) ;
#4174=EDGE_CURVE ( 'NONE', #2464, #7550, #2408, .T. ) ;
#4178=ORIENTED_EDGE ( 'NONE', *, *, #4709, .T. ) ;
#4179=FACE_OUTER_BOUND ( 'NONE', #4847, .T. ) ;
#4184=CARTESIAN_POINT ( 'NONE',  ( 13.93877027101358124, -218.0630240738406087, 94.58489134182006808 ) ) ;
#4197=CIRCLE ( 'NONE', #1605, 6.000000000000000000 ) ;
#4205=MECHANICAL_DESIGN_GEOMETRIC_PRESENTATION_REPRESENTATION('',(#7145),#4514);
#4206=ORIENTED_EDGE ( 'NONE', *, *, #7514, .F. ) ;
#4207=ORIENTED_EDGE ( 'NONE', *, *, #7545, .T. ) ;
#4209=CARTESIAN_POINT ( 'NONE',  ( 27.08493024494318746, -223.4607234779399789, 79.16428349862680136 ) ) ;
#4215=ADVANCED_FACE ( 'NONE', ( #7204, #5440, #2471 ), #4828, .F. ) ;
#4220=CARTESIAN_POINT ( 'NONE',  ( 14.29503225977587633, -218.0630240738405803, 94.45153243777278362 ) ) ;
#4225=CYLINDRICAL_SURFACE ( 'NONE', #4702, 8.000000000000028422 ) ;
#4227=CARTESIAN_POINT ( 'NONE',  ( 10.32550510630198737, -219.7296907405018089, 95.50346929579330890 ) ) ;
#4228=CARTESIAN_POINT ( 'NONE',  ( -21.50000000000000000, -215.0630240738404950, 94.68061005248806339 ) ) ;
#4238=LINE ( 'NONE', #6583, #870 ) ;
#4247=CARTESIAN_POINT ( 'NONE',  ( 27.12218822116579631, -221.8025471834170048, 78.75851208262513126 ) ) ;
#4249=EDGE_CURVE ( 'NONE', #877, #1926, #167, .T. ) ;
#4261=ORIENTED_EDGE ( 'NONE', *, *, #3005, .F. ) ;
#4269=ORIENTED_EDGE ( 'NONE', *, *, #3084, .T. ) ;
#4273=LINE ( 'NONE', #2494, #4119 ) ;
#4280=DIRECTION ( 'NONE',  ( -5.254869241218064794E-46, 0.7071067811865464625, -0.7071067811865485719 ) ) ;
#4281=CARTESIAN_POINT ( 'NONE',  ( 17.66255603274094454, -217.0856944719845103, 71.67965750360849597 ) ) ;
#4287=ORIENTED_EDGE ( 'NONE', *, *, #833, .F. ) ;
#4291=( NAMED_UNIT ( * ) SI_UNIT ( $, .STERADIAN. ) SOLID_ANGLE_UNIT ( ) );
#4295=EDGE_CURVE ( 'NONE', #6417, #5692, #6271, .T. ) ;
#4296=ORIENTED_EDGE ( 'NONE', *, *, #449, .F. ) ;
#4303=EDGE_LOOP ( 'NONE', ( #397, #1668, #3692, #6284 ) ) ;
#4312=VERTEX_POINT ( 'NONE', #3400 ) ;
#4320=CARTESIAN_POINT ( 'NONE',  ( -16.49999999999996447, 0.000000000000000000, 0.000000000000000000 ) ) ;
#4322=VERTEX_POINT ( 'NONE', #4588 ) ;
#4323=CARTESIAN_POINT ( 'NONE',  ( -13.50000000000000355, 16.00000000000003553, 42.31370849898485886 ) ) ;
#4326=VERTEX_POINT ( 'NONE', #5623 ) ;
#4331=ORIENTED_EDGE ( 'NONE', *, *, #5136, .T. ) ;
#4340=FACE_OUTER_BOUND ( 'NONE', #3122, .T. ) ;
#4343=VECTOR ( 'NONE', #3598, 1000.000000000000000 ) ;
#4344=VERTEX_POINT ( 'NONE', #4467 ) ;
#4345=DIRECTION ( 'NONE',  ( -7.623657272262518365E-17, -0.7071067811865464625, 0.7071067811865486830 ) ) ;
#4347=DIRECTION ( 'NONE',  ( 0.000000000000000000, -1.000000000000000000, -1.221245327087672392E-15 ) ) ;
#4353=VECTOR ( 'NONE', #6148, 1000.000000000000000 ) ;
#4356=CARTESIAN_POINT ( 'NONE',  ( 17.70193531918452123, -219.7017882839736274, 72.38063772785838523 ) ) ;
#4374=DIRECTION ( 'NONE',  ( 0.000000000000000000, 1.301042606982602954E-15, -1.000000000000000000 ) ) ;
#4378=VERTEX_POINT ( 'NONE', #7384 ) ;
#4381=PLANE ( 'NONE',  #3756 ) ;
#4388=ORIENTED_EDGE ( 'NONE', *, *, #3226, .F. ) ;
#4394=ORIENTED_EDGE ( 'NONE', *, *, #4709, .F. ) ;
#4396=CARTESIAN_POINT ( 'NONE',  ( -16.50000000000000000, -214.0630240738404382, 70.86973541144034527 ) ) ;
#4397=ORIENTED_EDGE ( 'NONE', *, *, #5076, .T. ) ;
#4417=ORIENTED_EDGE ( 'NONE', *, *, #3130, .T. ) ;
#4428=CARTESIAN_POINT ( 'NONE',  ( -12.50000000000000355, -218.0630240738404382, 71.94153218116483117 ) ) ;
#4434=ORIENTED_EDGE ( 'NONE', *, *, #2440, .F. ) ;
#4451=VECTOR ( 'NONE', #1029, 1000.000000000000000 ) ;
#4464=DIRECTION ( 'NONE',  ( 0.000000000000000000, 0.000000000000000000, -1.000000000000000000 ) ) ;
#4467=CARTESIAN_POINT ( 'NONE',  ( -12.50000000000001066, -218.0630240738404950, 95.20959099461346398 ) ) ;
#4474=ORIENTED_EDGE ( 'NONE', *, *, #833, .T. ) ;
#4484=AXIS2_PLACEMENT_3D ( 'NONE', #5354, #2458, #1877 ) ;
#4489=DIRECTION ( 'NONE',  ( 1.751623080406021728E-46, -0.9848077530122080203, 0.1736481776669304977 ) ) ;
#4501=CARTESIAN_POINT ( 'NONE',  ( -21.49999999999999645, -219.7493155748557285, 95.50692968358183066 ) ) ;
#4506=VERTEX_POINT ( 'NONE', #4668 ) ;
#4514=( GEOMETRIC_REPRESENTATION_CONTEXT ( 3 ) GLOBAL_UNCERTAINTY_ASSIGNED_CONTEXT ( ( #3029 ) ) GLOBAL_UNIT_ASSIGNED_CONTEXT ( ( #1374, #4928, #1995 ) ) REPRESENTATION_CONTEXT ( 'NONE', 'WORKASPACE' ) );
#4518=VECTOR ( 'NONE', #6705, 1000.000000000000000 ) ;
#4527=LINE ( 'NONE', #7019, #1935 ) ;
#4528=DIRECTION ( 'NONE',  ( 0.000000000000000000, -1.000000000000000000, 0.000000000000000000 ) ) ;
#4536=ORIENTED_EDGE ( 'NONE', *, *, #1123, .F. ) ;
#4538=CARTESIAN_POINT ( 'NONE',  ( 10.03180245857092423, -218.0630240738404382, 71.94153218116483117 ) ) ;
#4547=ORIENTED_EDGE ( 'NONE', *, *, #3002, .F. ) ;
#4555=CARTESIAN_POINT ( 'NONE',  ( 21.50000000000000000, 7.347880794884119736E-16, -5.999999999999999112 ) ) ;
#4556=CLOSED_SHELL ( 'NONE', ( #2052, #6631, #6961, #4865, #7351, #4562, #2774, #4895, #2341, #1728, #3069, #1608, #1573, #1334, #5404, #475, #3085, #7338, #513, #1680, #1732, #4215, #1879, #6503, #2535, #2307, #3813, #1889, #473, #3293 ) ) ;
#4562=ADVANCED_FACE ( 'NONE', ( #2427 ), #1079, .F. ) ;
#4568=CARTESIAN_POINT ( 'NONE',  ( 21.13461073196587137, -223.0630240738404666, 87.73717528194333681 ) ) ;
#4577=CARTESIAN_POINT ( 'NONE',  ( -16.49999999999996447, 0.000000000000000000, 6.000000000000000888 ) ) ;
#4582=ORIENTED_EDGE ( 'NONE', *, *, #5414, .F. ) ;
#4583=LINE ( 'NONE', #1429, #4518 ) ;
#4585=ORIENTED_EDGE ( 'NONE', *, *, #5038, .T. ) ;
#4587=DIRECTION ( 'NONE',  ( 1.000000000000000000, 0.000000000000000000, 7.663350976776343357E-46 ) ) ;
#4588=CARTESIAN_POINT ( 'NONE',  ( 10.03180245857092423, -218.0630240738404382, 71.94153218116483117 ) ) ;
#4589=ORIENTED_EDGE ( 'NONE', *, *, #5509, .T. ) ;
#4592=CARTESIAN_POINT ( 'NONE',  ( 27.14230383934499002, -218.4648600334251682, 89.55655311265203977 ) ) ;
#4602=VECTOR ( 'NONE', #5646, 1000.000000000000000 ) ;
#4621=AXIS2_PLACEMENT_3D ( 'NONE', #2638, #3838, #6135 ) ;
#4637=CARTESIAN_POINT ( 'NONE',  ( 17.67236366837565953, -212.7665347604138617, 94.27567702561840690 ) ) ;
#4646=CIRCLE ( 'NONE', #5012, 5.999999999999999112 ) ;
#4647=DIRECTION ( 'NONE',  ( 0.000000000000000000, -1.000000000000000000, -1.221245327087672392E-15 ) ) ;
#4650=CARTESIAN_POINT ( 'NONE',  ( 21.50149794217480093, -218.0630240738406087, 83.70532250279403286 ) ) ;
#4652=CARTESIAN_POINT ( 'NONE',  ( -15.92209785380265608, -113.7796841263388501, 41.77968412633906325 ) ) ;
#4655=CARTESIAN_POINT ( 'NONE',  ( -10.49999999999996625, -60.68629150101523351, -11.31370849898472031 ) ) ;
#4656=CARTESIAN_POINT ( 'NONE',  ( -16.49999999999996447, -49.37258300203045280, -2.775557561562891351E-14 ) ) ;
#4657=CARTESIAN_POINT ( 'NONE',  ( -18.18629150101523706, -223.0630240738405234, 96.09122589815579829 ) ) ;
#4658=CARTESIAN_POINT ( 'NONE',  ( 10.39932558417664410, -221.3963574071637197, 95.79734759697325330 ) ) ;
#4668=CARTESIAN_POINT ( 'NONE',  ( -16.49999999999996447, 6.938893903907228378E-15, -16.00000000000001421 ) ) ;
#4672=CARTESIAN_POINT ( 'NONE',  ( 21.50000000000000000, -60.68629150101523351, -11.31370849898472031 ) ) ;
#4673=CARTESIAN_POINT ( 'NONE',  ( 27.04900473833201957, -222.6575489669630770, 90.39048551345003091 ) ) ;
#4674=ORIENTED_EDGE ( 'NONE', *, *, #5413, .F. ) ;
#4686=CARTESIAN_POINT ( 'NONE',  ( 17.02959548118919031, -223.0630240738405234, 93.94559367446881026 ) ) ;
#4687=CARTESIAN_POINT ( 'NONE',  ( -21.50000000000000000, -69.31370849898461017, 42.31370849898474518 ) ) ;
#4692=ORIENTED_EDGE ( 'NONE', *, *, #5314, .F. ) ;
#4702=AXIS2_PLACEMENT_3D ( 'NONE', #5492, #6534, #7142 ) ;
#4709=EDGE_CURVE ( 'NONE', #628, #2172, #957, .T. ) ;
#4710=VERTEX_POINT ( 'NONE', #5417 ) ;
#4713=CARTESIAN_POINT ( 'NONE',  ( -10.49999999999996803, 7.347880794884121708E-16, -6.000000000000000888 ) ) ;
#4714=CARTESIAN_POINT ( 'NONE',  ( 26.99135978879997566, -227.6251019015761301, 80.18334626974973389 ) ) ;
#4722=FACE_OUTER_BOUND ( 'NONE', #3436, .T. ) ;
#4725=CARTESIAN_POINT ( 'NONE',  ( 14.95763687199172054, -223.0630240738405519, 95.12286150347453884 ) ) ;
#4742=EDGE_CURVE ( 'NONE', #6255, #1259, #2164, .T. ) ;
#4745=DIRECTION ( 'NONE',  ( 0.000000000000000000, 0.000000000000000000, 1.000000000000000000 ) ) ;
#4756=CARTESIAN_POINT ( 'NONE',  ( 10.10580595754474764, -214.7694783647500287, 94.62885002390419231 ) ) ;
#4760=ORIENTED_EDGE ( 'NONE', *, *, #6156, .F. ) ;
#4761=AXIS2_PLACEMENT_3D ( 'NONE', #6257, #1561, #5035 ) ;
#4774=CARTESIAN_POINT ( 'NONE',  ( -10.49999999999998579, -61.67366827531365203, 34.67366827531376572 ) ) ;
#4777=AXIS2_PLACEMENT_3D ( 'NONE', #7036, #2920, #4745 ) ;
#4790=CARTESIAN_POINT ( 'NONE',  ( 17.68960140267981984, -218.8824061789507880, 72.16108495452550642 ) ) ;
#4797=DIRECTION ( 'NONE',  ( 0.7071067811865435759, -8.465450562766819607E-16, 0.7071067811865514585 ) ) ;
#4803=PLANE ( 'NONE',  #2658 ) ;
#4809=AXIS2_PLACEMENT_3D ( 'NONE', #4976, #7316, #3058 ) ;
#4817=LINE ( 'NONE', #652, #2842 ) ;
#4819=AXIS2_PLACEMENT_3D ( 'NONE', #6508, #1924, #6616 ) ;
#4825=CARTESIAN_POINT ( 'NONE',  ( 10.43756829269602804, -227.0484711946324126, 74.34917548081359939 ) ) ;
#4828=PLANE ( 'NONE',  #75 ) ;
#4829=CIRCLE ( 'NONE', #639, 15.99999999999999645 ) ;
#4847=EDGE_LOOP ( 'NONE', ( #838, #1481, #4394, #6926, #165 ) ) ;
#4849=DIRECTION ( 'NONE',  ( 0.000000000000000000, -1.000000000000000000, -1.221245327087672392E-15 ) ) ;
#4865=ADVANCED_FACE ( 'NONE', ( #6891 ), #6398, .F. ) ;
#4866=ORIENTED_EDGE ( 'NONE', *, *, #3002, .T. ) ;
#4877=EDGE_CURVE ( 'NONE', #4322, #5235, #2659, .T. ) ;
#4880=FACE_OUTER_BOUND ( 'NONE', #390, .T. ) ;
#4887=ORIENTED_EDGE ( 'NONE', *, *, #1342, .T. ) ;
#4895=ADVANCED_FACE ( 'NONE', ( #3704 ), #6589, .F. ) ;
#4899=ORIENTED_EDGE ( 'NONE', *, *, #1361, .F. ) ;
#4903=EDGE_LOOP ( 'NONE', ( #1696, #6444 ) ) ;
#4906=DIRECTION ( 'NONE',  ( 0.000000000000000000, 0.000000000000000000, 1.000000000000000000 ) ) ;
#4918=DIRECTION ( 'NONE',  ( -1.000000000000000000, 4.067564042545842122E-31, -3.379803290564626122E-16 ) ) ;
#4921=VERTEX_POINT ( 'NONE', #6553 ) ;
#4922=ORIENTED_EDGE ( 'NONE', *, *, #5038, .F. ) ;
#4928=( NAMED_UNIT ( * ) PLANE_ANGLE_UNIT ( ) SI_UNIT ( $, .RADIAN. ) );
#4939=LINE ( 'NONE', #313, #7139 ) ;
#4940=DIRECTION ( 'NONE',  ( -1.078147950931789757E-16, 0.000000000000000000, 1.000000000000000000 ) ) ;
#4943=DIRECTION ( 'NONE',  ( 0.000000000000000000, 0.000000000000000000, 1.000000000000000000 ) ) ;
#4968=EDGE_CURVE ( 'NONE', #3465, #2464, #699, .T. ) ;
#4976=CARTESIAN_POINT ( 'NONE',  ( -16.49999999999998579, -125.0933926253236308, 30.46597562735434295 ) ) ;
#4977=AXIS2_PLACEMENT_3D ( 'NONE', #1962, #2115, #4464 ) ;
#5002=VERTEX_POINT ( 'NONE', #4713 ) ;
#5012=AXIS2_PLACEMENT_3D ( 'NONE', #7240, #318, #279 ) ;
#5018=FACE_OUTER_BOUND ( 'NONE', #2985, .T. ) ;
#5035=DIRECTION ( 'NONE',  ( -7.663350976776344912E-46, 0.000000000000000000, -1.000000000000000000 ) ) ;
#5038=EDGE_CURVE ( 'NONE', #687, #2809, #2197, .T. ) ;
#5041=ORIENTED_EDGE ( 'NONE', *, *, #2114, .T. ) ;
#5045=DIRECTION ( 'NONE',  ( 0.000000000000000000, 0.000000000000000000, -1.000000000000000000 ) ) ;
#5066=VECTOR ( 'NONE', #6895, 1000.000000000000000 ) ;
#5076=EDGE_CURVE ( 'NONE', #4326, #551, #236, .T. ) ;
#5077=EDGE_CURVE ( 'NONE', #6591, #2069, #3275, .T. ) ;
#5104=DIRECTION ( 'NONE',  ( -0.6427876096865581257, 9.159339953157541458E-16, -0.7660444431189622483 ) ) ;
#5105=DIRECTION ( 'NONE',  ( 0.000000000000000000, 0.000000000000000000, -1.000000000000000000 ) ) ;
#5117=DIRECTION ( 'NONE',  ( -0.6444004775717538935, -0.5407162030609466985, 0.5407162030609482528 ) ) ;
#5131=VECTOR ( 'NONE', #4647, 1000.000000000000000 ) ;
#5135=ORIENTED_EDGE ( 'NONE', *, *, #6060, .F. ) ;
#5136=EDGE_CURVE ( 'NONE', #4506, #162, #1893, .T. ) ;
#5146=( BOUNDED_SURFACE ( )  B_SPLINE_SURFACE ( 5, 3, ( 
 ( #1157, #2287, #7583, #543, #6514, #1661, #4132, #2320, #7045, #2392, #7542, #4756, #6437, #5203, #1736, #3595 ),
 ( #1195, #5894, #621, #2970, #2894, #3518, #3442, #5861, #7090, #4171, #5317, #2246, #5783, #4637, #583, #5245 ),
 ( #1235, #504, #6365, #2854, #4673, #2814, #5166, #3476, #7506, #4592, #6976, #6399, #7010, #2929, #7, #2356 ),
 ( #4714, #7273, #206, #2002, #130, #4209, #3121, #4247, #2505, #1888, #237, #3055, #3781, #1931, #700, #733 ),
 ( #5399, #3743, #7200, #6047, #1380, #2466, #1853, #93, #6590, #5512, #6554, #4356, #4790, #2433, #1313, #4281 ),
 ( #6698, #7161, #661, #4825, #3012, #2547, #3671, #7124, #6009, #6658, #164, #1273, #6084, #809, #1424, #3089 ) ),
 .UNSPECIFIED., .F., .F., .T. ) 
 B_SPLINE_SURFACE_WITH_KNOTS ( ( 6, 6 ),
 ( 4, 2, 2, 2, 2, 2, 2, 4 ),
 ( 0.000000000000000000, 1.000000000000000000 ),
 ( -1.150125124083905659, -0.9546592037126467867, -0.4819498650540673390, 0.000000000000000000, 0.02616758540912784634, 0.5083707369372295615, 0.9999999999999414912, 1.195465920371200363 ),
 .UNSPECIFIED. ) 
 GEOMETRIC_REPRESENTATION_ITEM ( )  RATIONAL_B_SPLINE_SURFACE ( (
 ( 1.000000000000000000, 1.000000000000000000, 1.000000000000000000, 1.000000000000000000, 1.000000000000000000, 1.000000000000000000, 1.000000000000000000, 1.000000000000000000, 1.000000000000000000, 1.000000000000000000, 1.000000000000000000, 1.000000000000000000, 1.000000000000000000, 1.000000000000000000, 1.000000000000000000, 1.000000000000000000),
 ( 0.5999999999999995337, 0.5999999999999995337, 0.5999999999999999778, 0.5999999999999999778, 0.5999999999999999778, 0.5999999999999999778, 0.5999999999999999778, 0.5999999999999999778, 0.5999999999999995337, 0.5999999999999995337, 0.5999999999999999778, 0.5999999999999999778, 0.5999999999999989786, 0.5999999999999989786, 0.5999999999999995337, 0.5999999999999995337),
 ( 0.3999999999999993561, 0.3999999999999993561, 0.4000000000000000777, 0.4000000000000000777, 0.4000000000000000777, 0.4000000000000000777, 0.4000000000000000777, 0.4000000000000000777, 0.3999999999999993561, 0.3999999999999993561, 0.4000000000000000777, 0.4000000000000000777, 0.3999999999999984679, 0.3999999999999984679, 0.3999999999999993561, 0.3999999999999993561),
 ( 0.3999999999999993561, 0.3999999999999993561, 0.4000000000000000777, 0.4000000000000000777, 0.4000000000000000777, 0.4000000000000000777, 0.4000000000000000777, 0.4000000000000000777, 0.3999999999999993561, 0.3999999999999993561, 0.4000000000000000777, 0.4000000000000000777, 0.3999999999999984679, 0.3999999999999984679, 0.3999999999999993561, 0.3999999999999993561),
 ( 0.5999999999999995337, 0.5999999999999995337, 0.5999999999999999778, 0.5999999999999999778, 0.5999999999999999778, 0.5999999999999999778, 0.5999999999999999778, 0.5999999999999999778, 0.5999999999999995337, 0.5999999999999995337, 0.5999999999999999778, 0.5999999999999999778, 0.5999999999999989786, 0.5999999999999989786, 0.5999999999999995337, 0.5999999999999995337),
 ( 1.000000000000000000, 1.000000000000000000, 1.000000000000000000, 1.000000000000000000, 1.000000000000000000, 1.000000000000000000, 1.000000000000000000, 1.000000000000000000, 1.000000000000000000, 1.000000000000000000, 1.000000000000000000, 1.000000000000000000, 1.000000000000000000, 1.000000000000000000, 1.000000000000000000, 1.000000000000000000) ) ) 
 REPRESENTATION_ITEM ( '' )  SURFACE ( )  );
#5150=DIRECTION ( 'NONE',  ( 0.000000000000000000, 0.000000000000000000, 1.000000000000000000 ) ) ;
#5153=CARTESIAN_POINT ( 'NONE',  ( -16.49999999999998934, -71.76505905230354188, 44.76505905230365556 ) ) ;
#5166=CARTESIAN_POINT ( 'NONE',  ( 27.10306686690893940, -220.2280969603149003, 89.90726370123081779 ) ) ;
#5196=EDGE_LOOP ( 'NONE', ( #7344, #5517, #1875, #2901 ) ) ;
#5203=CARTESIAN_POINT ( 'NONE',  ( 10.01709100512437267, -212.7665347604136343, 94.27567702562227225 ) ) ;
#5212=CYLINDRICAL_SURFACE ( 'NONE', #5252, 15.99999999999997335 ) ;
#5213=AXIS2_PLACEMENT_3D ( 'NONE', #1930, #2504, #4280 ) ;
#5218=CARTESIAN_POINT ( 'NONE',  ( 21.18129193964234958, -223.0630240738404950, 81.69876281950602959 ) ) ;
#5224=EDGE_LOOP ( 'NONE', ( #6809, #1333, #1646, #6342 ) ) ;
#5230=VECTOR ( 'NONE', #4489, 1000.000000000000114 ) ;
#5231=CARTESIAN_POINT ( 'NONE',  ( 21.50000000000000000, -223.0630240738404382, 73.28127814332047762 ) ) ;
#5235=VERTEX_POINT ( 'NONE', #7423 ) ;
#5245=CARTESIAN_POINT ( 'NONE',  ( 17.66255603274094454, -212.1022451272886542, 94.15854484029739524 ) ) ;
#5252=AXIS2_PLACEMENT_3D ( 'NONE', #7478, #1623, #7515 ) ;
#5256=CARTESIAN_POINT ( 'NONE',  ( 18.38715965971085353, -218.0630240738404950, 75.65381970816498836 ) ) ;
#5261=ORIENTED_EDGE ( 'NONE', *, *, #4249, .T. ) ;
#5262=EDGE_LOOP ( 'NONE', ( #1767, #250, #7287, #844 ) ) ;
#5274=EDGE_CURVE ( 'NONE', #5684, #3448, #4008, .T. ) ;
#5276=DIRECTION ( 'NONE',  ( -8.747574602982985342E-17, -0.9659258262890683122, 0.2588190451025207950 ) ) ;
#5284=DIRECTION ( 'NONE',  ( -1.000000000000000000, 1.294224922628222493E-31, -1.078147950931789264E-16 ) ) ;
#5288=PLANE ( 'NONE',  #3131 ) ;
#5290=CARTESIAN_POINT ( 'NONE',  ( 18.25938667636025059, -218.0630240738405234, 75.51685001270919884 ) ) ;
#5291=CARTESIAN_POINT ( 'NONE',  ( 20.45699128574564085, -223.0630240738404666, 89.66439215578999722 ) ) ;
#5304=ORIENTED_EDGE ( 'NONE', *, *, #7262, .T. ) ;
#5314=EDGE_CURVE ( 'NONE', #2069, #4378, #6884, .T. ) ;
#5317=CARTESIAN_POINT ( 'NONE',  ( 17.72636667137882682, -216.4242598635584613, 94.92063264932014022 ) ) ;
#5327=CARTESIAN_POINT ( 'NONE',  ( 21.28788537653265323, -218.0630240738404666, 86.14873225104479104 ) ) ;
#5328=AXIS2_PLACEMENT_3D ( 'NONE', #1404, #4918, #3689 ) ;
#5340=CARTESIAN_POINT ( 'NONE',  ( -13.35769912250762914, -65.39789427971170710, 38.39789427971182789 ) ) ;
#5353=( BOUNDED_CURVE ( )  B_SPLINE_CURVE ( 3, ( #763, #1266, #159, #2348 ),
 .UNSPECIFIED., .F., .T. ) 
 B_SPLINE_CURVE_WITH_KNOTS ( ( 4, 4 ),
 ( 4.712388980384686121, 5.585053606381841895 ),
 .UNSPECIFIED. ) 
 CURVE ( )  GEOMETRIC_REPRESENTATION_ITEM ( )  RATIONAL_B_SPLINE_CURVE ( ( 1.000000000000000000, 0.9375385246911012160, 0.9375385246911012160, 1.000000000000000000 ) ) 
 REPRESENTATION_ITEM ( '' )  );
#5354=CARTESIAN_POINT ( 'NONE',  ( 21.50000000000000000, -49.37258300203045280, -2.775557561562891351E-14 ) ) ;
#5399=CARTESIAN_POINT ( 'NONE',  ( 17.83909347413333890, -228.8136496942591975, 74.82215363428539945 ) ) ;
#5404=ADVANCED_FACE ( 'NONE', ( #724 ), #1921, .T. ) ;
#5413=EDGE_CURVE ( 'NONE', #4312, #4326, #4273, .T. ) ;
#5414=EDGE_CURVE ( 'NONE', #7581, #2056, #2921, .T. ) ;
#5417=CARTESIAN_POINT ( 'NONE',  ( -16.50000000000000355, -99.90626354475340065, 72.90626354475362803 ) ) ;
#5426=LINE ( 'NONE', #263, #6595 ) ;
#5440=FACE_BOUND ( 'NONE', #5979, .T. ) ;
#5441=VECTOR ( 'NONE', #1418, 1000.000000000000000 ) ;
#5444=DIRECTION ( 'NONE',  ( -1.000000000000000000, 0.000000000000000000, -7.663350976776343357E-46 ) ) ;
#5446=( LENGTH_UNIT ( ) NAMED_UNIT ( * ) SI_UNIT ( .MILLI., .METRE. ) );
#5454=CARTESIAN_POINT ( 'NONE',  ( -21.48215622306531003, -113.7796841263388501, 41.77968412633906325 ) ) ;
#5456=CARTESIAN_POINT ( 'NONE',  ( -13.49999999999999822, -223.0630240738404382, 73.28127814332047762 ) ) ;
#5473=VECTOR ( 'NONE', #977, 1000.000000000000000 ) ;
#5475=CARTESIAN_POINT ( 'NONE',  ( -16.49999999999996447, -99.90626354475340065, 72.90626354475362803 ) ) ;
#5484=CARTESIAN_POINT ( 'NONE',  ( -18.18629150101523351, -223.0630240738404382, 73.28127814332044920 ) ) ;
#5492=CARTESIAN_POINT ( 'NONE',  ( -24.50000000000000000, 16.00000000000006395, 30.68629150101531877 ) ) ;
#5495=DIRECTION ( 'NONE',  ( -3.379803290564628095E-16, -1.221245327087672392E-15, 1.000000000000000000 ) ) ;
#5502=VECTOR ( 'NONE', #2085, 1000.000000000000000 ) ;
#5504=CARTESIAN_POINT ( 'NONE',  ( -16.50000000000000355, -214.0630240738404382, 71.94153218116485959 ) ) ;
#5509=EDGE_CURVE ( 'NONE', #2575, #238, #2107, .T. ) ;
#5511=CARTESIAN_POINT ( 'NONE',  ( -16.50000000000000000, -216.4061698243480976, 71.49757942303727987 ) ) ;
#5512=CARTESIAN_POINT ( 'NONE',  ( 17.73846410710429211, -222.1285142276679210, 73.03087698472572242 ) ) ;
#5517=ORIENTED_EDGE ( 'NONE', *, *, #5931, .T. ) ;
#5518=FACE_OUTER_BOUND ( 'NONE', #4303, .T. ) ;
#5527=DIRECTION ( 'NONE',  ( -1.000000000000000000, 4.067564042545842122E-31, -3.379803290564627601E-16 ) ) ;
#5530=CYLINDRICAL_SURFACE ( 'NONE', #2702, 4.000000000000003553 ) ;
#5553=DIRECTION ( 'NONE',  ( -1.000000000000000000, 0.000000000000000000, -7.663350976776343357E-46 ) ) ;
#5565=LINE ( 'NONE', #974, #7211 ) ;
#5572=ORIENTED_EDGE ( 'NONE', *, *, #4174, .T. ) ;
#5576=LINE ( 'NONE', #5504, #1612 ) ;
#5602=EDGE_LOOP ( 'NONE', ( #1274, #2088, #5261, #490 ) ) ;
#5614=FACE_OUTER_BOUND ( 'NONE', #5196, .T. ) ;
#5623=CARTESIAN_POINT ( 'NONE',  ( -16.49999999999996447, -45.34314575050758123, 18.34314575050765939 ) ) ;
#5628=ORIENTED_EDGE ( 'NONE', *, *, #6378, .F. ) ;
#5633=ORIENTED_EDGE ( 'NONE', *, *, #5796, .T. ) ;
#5635=LINE ( 'NONE', #3798, #698 ) ;
#5638=CARTESIAN_POINT ( 'NONE',  ( -21.50000000000000000, -69.31370849898461017, 42.31370849898474518 ) ) ;
#5640=CARTESIAN_POINT ( 'NONE',  ( -16.47169665601479949, -116.3958977277557523, 43.92260702357706492 ) ) ;
#5646=DIRECTION ( 'NONE',  ( -1.000000000000000000, 0.000000000000000000, -7.663350976776343357E-46 ) ) ;
#5647=CARTESIAN_POINT ( 'NONE',  ( 21.50000000000000000, -105.5631177942458265, 67.24940929526127320 ) ) ;
#5649=CARTESIAN_POINT ( 'NONE',  ( -10.49999999999997513, -104.2695387347598057, 32.26953873475996204 ) ) ;
#5652=ORIENTED_EDGE ( 'NONE', *, *, #5796, .F. ) ;
#5660=AXIS2_PLACEMENT_3D ( 'NONE', #324, #6130, #4374 ) ;
#5668=CARTESIAN_POINT ( 'NONE',  ( -13.49999999999999822, -215.0630240738404382, 73.28127814332047762 ) ) ;
#5677=CARTESIAN_POINT ( 'NONE',  ( -16.49999999999996447, 0.000000000000000000, 0.000000000000000000 ) ) ;
#5684=VERTEX_POINT ( 'NONE', #7527 ) ;
#5688=LINE ( 'NONE', #2758, #6081 ) ;
#5692=VERTEX_POINT ( 'NONE', #3462 ) ;
#5715=VECTOR ( 'NONE', #4528, 1000.000000000000000 ) ;
#5717=CARTESIAN_POINT ( 'NONE',  ( -21.35140889653590790, -111.8253808406378624, 39.82538084063802586 ) ) ;
#5724=( GEOMETRIC_REPRESENTATION_CONTEXT ( 3 ) GLOBAL_UNCERTAINTY_ASSIGNED_CONTEXT ( ( #637 ) ) GLOBAL_UNIT_ASSIGNED_CONTEXT ( ( #5446, #3064, #4291 ) ) REPRESENTATION_CONTEXT ( 'NONE', 'WORKASPACE' ) );
#5733=DIRECTION ( 'NONE',  ( 1.381786968815111140E-76, -1.000000000000000000, -1.221245327087672392E-15 ) ) ;
#5742=CARTESIAN_POINT ( 'NONE',  ( 21.50000000000000000, -223.0630240738404666, 96.09122589815579829 ) ) ;
#5756=FACE_OUTER_BOUND ( 'NONE', #1448, .T. ) ;
#5759=CARTESIAN_POINT ( 'NONE',  ( 17.65194526459429625, -223.0630240738404098, 76.13224682984757408 ) ) ;
#5772=CARTESIAN_POINT ( 'NONE',  ( -18.84314575050759188, -108.3431457505073752, 36.34314575050756702 ) ) ;
#5783=CARTESIAN_POINT ( 'NONE',  ( 17.68960140267981984, -213.9340789708221564, 94.48154657109715515 ) ) ;
#5789=VERTEX_POINT ( 'NONE', #1180 ) ;
#5795=CARTESIAN_POINT ( 'NONE',  ( 21.49983462661594658, -218.0630240738406087, 83.89749897642222720 ) ) ;
#5796=EDGE_CURVE ( 'NONE', #6417, #3729, #6872, .T. ) ;
#5797=CARTESIAN_POINT ( 'NONE',  ( 17.23587211895880955, -223.0630240738404098, 75.76440619659675235 ) ) ;
#5808=ORIENTED_EDGE ( 'NONE', *, *, #2261, .T. ) ;
#5814=ORIENTED_EDGE ( 'NONE', *, *, #5414, .T. ) ;
#5830=CARTESIAN_POINT ( 'NONE',  ( -21.48215622306531003, -113.7796841263388501, 41.77968412633906325 ) ) ;
#5834=AXIS2_PLACEMENT_3D ( 'NONE', #2586, #3132, #4906 ) ;
#5835=CARTESIAN_POINT ( 'NONE',  ( 16.32211914470424574, -218.0630240738405519, 93.45296875943058978 ) ) ;
#5861=CARTESIAN_POINT ( 'NONE',  ( 17.75187451922245430, -218.1519544391847489, 95.22527181742790958 ) ) ;
#5872=CARTESIAN_POINT ( 'NONE',  ( 19.77324663291341622, -218.0630240738404950, 77.42037680107310393 ) ) ;
#5894=CARTESIAN_POINT ( 'NONE',  ( 17.83418965632456121, -223.7273137069674931, 96.20835808347007401 ) ) ;
#5904=CARTESIAN_POINT ( 'NONE',  ( 18.63742165201374945, -218.0630240738404666, 75.93507306776972143 ) ) ;
#5905=CARTESIAN_POINT ( 'NONE',  ( 21.42066185573919412, -223.0630240738404666, 86.48599461439638958 ) ) ;
#5917=( BOUNDED_CURVE ( )  B_SPLINE_CURVE ( 3, ( #1589, #3877, #2675, #332 ),
 .UNSPECIFIED., .F., .T. ) 
 B_SPLINE_CURVE_WITH_KNOTS ( ( 4, 4 ),
 ( -1.776356839400250465E-15, 1.570796326794894782 ),
 .UNSPECIFIED. ) 
 CURVE ( )  GEOMETRIC_REPRESENTATION_ITEM ( )  RATIONAL_B_SPLINE_CURVE ( ( 1.000000000000000000, 0.8047378541243649375, 0.8047378541243649375, 1.000000000000000000 ) ) 
 REPRESENTATION_ITEM ( '' )  );
#5928=ORIENTED_EDGE ( 'NONE', *, *, #1495, .T. ) ;
#5931=EDGE_CURVE ( 'NONE', #238, #4710, #2503, .T. ) ;
#5942=CARTESIAN_POINT ( 'NONE',  ( 21.45574242475734650, -218.0630240738404950, 84.84425821389238820 ) ) ;
#5964=VERTEX_POINT ( 'NONE', #5638 ) ;
#5979=EDGE_LOOP ( 'NONE', ( #7248, #3397 ) ) ;
#5993=CARTESIAN_POINT ( 'NONE',  ( -21.50000000000000000, -215.0630240738403813, -2.498001805406602216E-13 ) ) ;
#5998=ORIENTED_EDGE ( 'NONE', *, *, #3711, .F. ) ;
#6006=ORIENTED_EDGE ( 'NONE', *, *, #1670, .T. ) ;
#6009=CARTESIAN_POINT ( 'NONE',  ( 10.25365409304695952, -222.9757987891379400, 73.25790619872482523 ) ) ;
#6010=ORIENTED_EDGE ( 'NONE', *, *, #7457, .T. ) ;
#6014=PLANE ( 'NONE',  #1816 ) ;
#6025=CIRCLE ( 'NONE', #985, 15.99999999999997691 ) ;
#6036=ORIENTED_EDGE ( 'NONE', *, *, #1851, .F. ) ;
#6047=CARTESIAN_POINT ( 'NONE',  ( 17.81252276423129999, -227.0484711946332936, 74.34917548081020300 ) ) ;
#6050=CARTESIAN_POINT ( 'NONE',  ( -10.49999999999997513, 16.00000000000006750, 32.26953873476009704 ) ) ;
#6060=EDGE_CURVE ( 'NONE', #3729, #4322, #6955, .T. ) ;
#6072=VECTOR ( 'NONE', #6649, 1000.000000000000114 ) ;
#6081=VECTOR ( 'NONE', #5117, 1000.000000000000000 ) ;
#6084=CARTESIAN_POINT ( 'NONE',  ( 10.06880420804609422, -218.8824061789517259, 72.16108495452192528 ) ) ;
#6090=CARTESIAN_POINT ( 'NONE',  ( 21.50000000000000000, -49.37258300203045280, 5.999999999999972466 ) ) ;
#6116=ORIENTED_EDGE ( 'NONE', *, *, #4877, .T. ) ;
#6120=EDGE_CURVE ( 'NONE', #4312, #5684, #7415, .T. ) ;
#6122=DIRECTION ( 'NONE',  ( -1.000000000000000000, 0.000000000000000000, -7.663350976776343357E-46 ) ) ;
#6128=( BOUNDED_CURVE ( )  B_SPLINE_CURVE ( 3, ( #5340, #3573, #4774, #7110 ),
 .UNSPECIFIED., .F., .T. ) 
 B_SPLINE_CURVE_WITH_KNOTS ( ( 4, 4 ),
 ( 0.6981317007977386746, 1.570796326794897446 ),
 .UNSPECIFIED. ) 
 CURVE ( )  GEOMETRIC_REPRESENTATION_ITEM ( )  RATIONAL_B_SPLINE_CURVE ( ( 1.000000000000000000, 0.9375385246911008830, 0.9375385246911008830, 1.000000000000000000 ) ) 
 REPRESENTATION_ITEM ( '' )  );
#6130=DIRECTION ( 'NONE',  ( 0.000000000000000000, -1.000000000000000000, -1.221245327087672392E-15 ) ) ;
#6131=CARTESIAN_POINT ( 'NONE',  ( 21.50000000000000000, -49.37258300203045280, -2.775557561562891351E-14 ) ) ;
#6135=DIRECTION ( 'NONE',  ( 0.000000000000000000, 0.000000000000000000, 1.000000000000000000 ) ) ;
#6138=CARTESIAN_POINT ( 'NONE',  ( -10.49999999999996803, -49.37258300203045280, -2.775557561562891351E-14 ) ) ;
#6139=ORIENTED_EDGE ( 'NONE', *, *, #7186, .F. ) ;
#6147=VERTEX_POINT ( 'NONE', #3303 ) ;
#6148=DIRECTION ( 'NONE',  ( 5.254869241218065572E-46, -0.7071067811865465735, 0.7071067811865485719 ) ) ;
#6150=CIRCLE ( 'NONE', #4819, 7.999999999999986677 ) ;
#6156=EDGE_CURVE ( 'NONE', #3448, #162, #373, .T. ) ;
#6172=DIRECTION ( 'NONE',  ( -1.000000000000000000, 0.000000000000000000, -7.663350976776343357E-46 ) ) ;
#6175=CARTESIAN_POINT ( 'NONE',  ( -21.50000000000000000, -120.9522879036832848, 45.92078884797942351 ) ) ;
#6180=AXIS2_PLACEMENT_3D ( 'NONE', #2933, #5284, #51 ) ;
#6185=DIRECTION ( 'NONE',  ( 0.6444004775717538935, 0.5407162030609466985, -0.5407162030609481418 ) ) ;
#6198=VERTEX_POINT ( 'NONE', #3384 ) ;
#6202=FACE_OUTER_BOUND ( 'NONE', #6551, .T. ) ;
#6208=ORIENTED_EDGE ( 'NONE', *, *, #3005, .T. ) ;
#6215=CARTESIAN_POINT ( 'NONE',  ( -16.16037543966235646, -114.3720785834762665, 42.37207858347650102 ) ) ;
#6217=ORIENTED_EDGE ( 'NONE', *, *, #2739, .F. ) ;
#6220=DIRECTION ( 'NONE',  ( -3.503246160812044233E-46, 0.9659258262890683122, -0.2588190451025208505 ) ) ;
#6226=ORIENTED_EDGE ( 'NONE', *, *, #7514, .T. ) ;
#6255=VERTEX_POINT ( 'NONE', #4655 ) ;
#6257=CARTESIAN_POINT ( 'NONE',  ( -16.49999999999996803, 16.00000000000012079, -15.99999999999995914 ) ) ;
#6271=LINE ( 'NONE', #5742, #2402 ) ;
#6284=ORIENTED_EDGE ( 'NONE', *, *, #7545, .F. ) ;
#6285=FACE_OUTER_BOUND ( 'NONE', #1097, .T. ) ;
#6323=AXIS2_PLACEMENT_3D ( 'NONE', #1284, #5444, #776 ) ;
#6328=EDGE_LOOP ( 'NONE', ( #4474, #4207 ) ) ;
#6342=ORIENTED_EDGE ( 'NONE', *, *, #4139, .T. ) ;
#6344=ORIENTED_EDGE ( 'NONE', *, *, #6685, .F. ) ;
#6349=EDGE_LOOP ( 'NONE', ( #2253, #4331, #4760, #4417 ) ) ;
#6353=LINE ( 'NONE', #2312, #6724 ) ;
#6355=CARTESIAN_POINT ( 'NONE',  ( -13.35769912250762204, 16.00000000000006750, 38.39789427971190605 ) ) ;
#6364=CARTESIAN_POINT ( 'NONE',  ( 10.10706597980996335, -219.7296907405071238, 72.38811416855006087 ) ) ;
#6365=CARTESIAN_POINT ( 'NONE',  ( 27.00607124224622169, -224.5869008243855944, 90.77423662209318422 ) ) ;
#6376=CARTESIAN_POINT ( 'NONE',  ( 18.87504319907951356, -223.0630240738404666, 92.12888099325203939 ) ) ;
#6378=EDGE_CURVE ( 'NONE', #162, #1669, #3330, .T. ) ;
#6385=PLANE ( 'NONE',  #7151 ) ;
#6386=ORIENTED_EDGE ( 'NONE', *, *, #7186, .T. ) ;
#6389=CYLINDRICAL_SURFACE ( 'NONE', #3424, 5.999999999999999112 ) ;
#6397=AXIS2_PLACEMENT_3D ( 'NONE', #6138, #1986, #2531 ) ;
#6398=PLANE ( 'NONE',  #905 ) ;
#6399=CARTESIAN_POINT ( 'NONE',  ( 27.19709702122541017, -216.0025558445558431, 89.06679694989070128 ) ) ;
#6408=PLANE ( 'NONE',  #3540 ) ;
#6409=CARTESIAN_POINT ( 'NONE',  ( -18.84314575050759544, 16.00000000000003908, 36.34314575050770202 ) ) ;
#6411=CARTESIAN_POINT ( 'NONE',  ( 15.03306249438985631, -218.0630240738404950, 73.12099198157908120 ) ) ;
#6416=EDGE_LOOP ( 'NONE', ( #2587, #4536, #2325, #7424 ) ) ;
#6417=VERTEX_POINT ( 'NONE', #1585 ) ;
#6422=CARTESIAN_POINT ( 'NONE',  ( -15.48397095257170974, -67.18204818810112045, 40.18204818810124124 ) ) ;
#6431=CARTESIAN_POINT ( 'NONE',  ( 21.50000000000000000, -39.68629150101519087, 15.99999999999998579 ) ) ;
#6433=VERTEX_POINT ( 'NONE', #6789 ) ;
#6437=CARTESIAN_POINT ( 'NONE',  ( 10.06880420804609422, -213.9340789708228669, 94.48154657108734966 ) ) ;
#6444=ORIENTED_EDGE ( 'NONE', *, *, #3403, .T. ) ;
#6453=CARTESIAN_POINT ( 'NONE',  ( 21.50932527815889728, -223.0630240738404666, 85.38297702798109867 ) ) ;
#6457=ORIENTED_EDGE ( 'NONE', *, *, #449, .T. ) ;
#6463=CARTESIAN_POINT ( 'NONE',  ( -10.49999999999996803, 0.000000000000000000, 5.999999999999999112 ) ) ;
#6485=LINE ( 'NONE', #1203, #5502 ) ;
#6487=ORIENTED_EDGE ( 'NONE', *, *, #1002, .T. ) ;
#6488=CARTESIAN_POINT ( 'NONE',  ( 17.77546999798919103, -218.0630240738405519, 92.26857489675208512 ) ) ;
#6489=CARTESIAN_POINT ( 'NONE',  ( 17.86619911493601620, -223.0630240738404666, 93.22347854821404667 ) ) ;
#6503=ADVANCED_FACE ( 'NONE', ( #4722 ), #5288, .F. ) ;
#6504=FACE_OUTER_BOUND ( 'NONE', #3010, .T. ) ;
#6508=CARTESIAN_POINT ( 'NONE',  ( -16.49999999999996447, -39.68629150101520509, 23.99999999999999289 ) ) ;
#6514=CARTESIAN_POINT ( 'NONE',  ( 10.40199052334513041, -221.4565245236570377, 95.80795668296244116 ) ) ;
#6515=EDGE_LOOP ( 'NONE', ( #7322, #6618, #6826, #6964, #6010, #7494, #2688, #4388 ) ) ;
#6521=FACE_OUTER_BOUND ( 'NONE', #2843, .T. ) ;
#6526=CARTESIAN_POINT ( 'NONE',  ( 18.04970750630426579, -218.0630240738405519, 92.00715684020322271 ) ) ;
#6529=PRODUCT ( 'left arm', 'left arm', '', ( #586 ) ) ;
#6534=DIRECTION ( 'NONE',  ( 0.000000000000000000, -1.000000000000000000, -1.221245327087672392E-15 ) ) ;
#6535=DIRECTION ( 'NONE',  ( -1.000000000000000000, 0.000000000000000000, -7.663350976776343357E-46 ) ) ;
#6547=ORIENTED_EDGE ( 'NONE', *, *, #5077, .T. ) ;
#6551=EDGE_LOOP ( 'NONE', ( #666, #1177, #89, #48 ) ) ;
#6553=CARTESIAN_POINT ( 'NONE',  ( -10.49999999999996803, -49.37258300203045280, -6.000000000000029310 ) ) ;
#6554=CARTESIAN_POINT ( 'NONE',  ( 17.72636667137882682, -221.3248423084426975, 72.81553374298033532 ) ) ;
#6561=CARTESIAN_POINT ( 'NONE',  ( 17.35616244728660718, -218.0630240738405519, 92.64882813447223953 ) ) ;
#6563=LINE ( 'NONE', #4104, #7245 ) ;
#6571=CARTESIAN_POINT ( 'NONE',  ( 21.50000000000000000, -223.0630240738404382, 73.28127814332047762 ) ) ;
#6574=VECTOR ( 'NONE', #1568, 1000.000000000000000 ) ;
#6583=CARTESIAN_POINT ( 'NONE',  ( -16.49999999999999289, -120.9522879036832848, 45.92078884797942351 ) ) ;
#6589=PLANE ( 'NONE',  #5213 ) ;
#6590=CARTESIAN_POINT ( 'NONE',  ( 17.75121803101545481, -222.9757987891384801, 73.25790619872466891 ) ) ;
#6591=VERTEX_POINT ( 'NONE', #7100 ) ;
#6595=VECTOR ( 'NONE', #4345, 999.9999999999998863 ) ;
#6599=FACE_OUTER_BOUND ( 'NONE', #6862, .T. ) ;
#6616=DIRECTION ( 'NONE',  ( 0.000000000000000000, -8.673617379884050263E-16, -1.000000000000000000 ) ) ;
#6618=ORIENTED_EDGE ( 'NONE', *, *, #5274, .F. ) ;
#6631=ADVANCED_FACE ( 'NONE', ( #3755 ), #3643, .F. ) ;
#6641=FACE_OUTER_BOUND ( 'NONE', #2079, .T. ) ;
#6649=DIRECTION ( 'NONE',  ( 5.868966822792466307E-17, 0.9848077530122080203, -0.1736481776669304977 ) ) ;
#6658=CARTESIAN_POINT ( 'NONE',  ( 10.21539232130207964, -222.1285142276787496, 73.03087698472252498 ) ) ;
#6665=DIRECTION ( 'NONE',  ( 0.000000000000000000, 1.301042606982607490E-15, -1.000000000000000000 ) ) ;
#6669=DIRECTION ( 'NONE',  ( 0.000000000000000000, 0.000000000000000000, 1.000000000000000000 ) ) ;
#6671=FACE_OUTER_BOUND ( 'NONE', #5602, .T. ) ;
#6675=CARTESIAN_POINT ( 'NONE',  ( -10.49999999999996980, 0.000000000000000000, -15.99999999999995914 ) ) ;
#6685=EDGE_CURVE ( 'NONE', #5002, #3211, #787, .T. ) ;
#6688=VECTOR ( 'NONE', #7152, 1000.000000000000000 ) ;
#6691=CARTESIAN_POINT ( 'NONE',  ( -21.50000000000000000, 16.00000000000003553, 42.31370849898488729 ) ) ;
#6697=CARTESIAN_POINT ( 'NONE',  ( -14.84314575050762564, -218.0630240738404666, 71.94153218116483117 ) ) ;
#6698=CARTESIAN_POINT ( 'NONE',  ( 10.51728042240002914, -228.8136496942592260, 74.82215363428539945 ) ) ;
#6705=DIRECTION ( 'NONE',  ( -1.000000000000000000, 0.000000000000000000, -7.663350976776343357E-46 ) ) ;
#6712=PRODUCT_DEFINITION_SHAPE ( 'NONE', 'NONE',  #4155 ) ;
#6724=VECTOR ( 'NONE', #4162, 1000.000000000000000 ) ;
#6789=CARTESIAN_POINT ( 'NONE',  ( -16.49999999999996447, 7.347880794884121708E-16, -6.000000000000000888 ) ) ;
#6794=DIRECTION ( 'NONE',  ( -1.000000000000000000, 0.000000000000000000, -7.663350976776343357E-46 ) ) ;
#6796=ORIENTED_EDGE ( 'NONE', *, *, #1937, .T. ) ;
#6809=ORIENTED_EDGE ( 'NONE', *, *, #4742, .T. ) ;
#6816=CARTESIAN_POINT ( 'NONE',  ( -15.42929891127140962, -112.5545107178312065, 40.55451071783137706 ) ) ;
#6822=CYLINDRICAL_SURFACE ( 'NONE', #3819, 8.000000000000007105 ) ;
#6826=ORIENTED_EDGE ( 'NONE', *, *, #6120, .F. ) ;
#6844=ORIENTED_EDGE ( 'NONE', *, *, #3041, .T. ) ;
#6856=VERTEX_POINT ( 'NONE', #3319 ) ;
#6859=CARTESIAN_POINT ( 'NONE',  ( 21.50000000000000000, -218.0630240738404950, 95.20959099461346398 ) ) ;
#6862=EDGE_LOOP ( 'NONE', ( #3738, #1188, #4674, #1615 ) ) ;
#6872=B_SPLINE_CURVE_WITH_KNOTS ( 'NONE', 3,
 ( #2913, #4658, #4227, #1257 ),
 .UNSPECIFIED., .F., .F.,
 ( 4, 4 ),
 ( 0.000000000000000000, 1.000000000000000000 ),
 .UNSPECIFIED. ) ;
#6876=LINE ( 'NONE', #6175, #2540 ) ;
#6879=CARTESIAN_POINT ( 'NONE',  ( -10.49999999999996803, 0.000000000000000000, 0.000000000000000000 ) ) ;
#6884=LINE ( 'NONE', #6355, #1520 ) ;
#6891=FACE_OUTER_BOUND ( 'NONE', #1815, .T. ) ;
#6895=DIRECTION ( 'NONE',  ( -1.000000000000000000, 0.000000000000000000, -7.663350976776343357E-46 ) ) ;
#6907=CARTESIAN_POINT ( 'NONE',  ( 13.40989346456145093, -223.0630240738405234, 95.79326762286926567 ) ) ;
#6926=ORIENTED_EDGE ( 'NONE', *, *, #2983, .F. ) ;
#6934=CARTESIAN_POINT ( 'NONE',  ( -21.50000000000000000, 0.000000000000000000, 0.000000000000000000 ) ) ;
#6951=CARTESIAN_POINT ( 'NONE',  ( 17.92438667413662046, -223.0630240738404950, 76.38511945211442367 ) ) ;
#6955=B_SPLINE_CURVE_WITH_KNOTS ( 'NONE', 3,
 ( #1791, #7136, #4145, #1866, #4184, #4220, #3487, #5835, #6561, #6488, #6526, #1248, #633, #1209, #2299, #3604, #3455, #17, #5327, #5942, #63, #5795, #4650, #557, #6984, #7593, #2905, #3564, #5872, #674, #5904, #5256, #5290, #2980, #4066, #3027, #6411, #1131, #7488, #3957, #1518, #1682, #4538 ),
 .UNSPECIFIED., .F., .F.,
 ( 4, 1, 2, 2, 1, 1, 2, 2, 1, 2, 2, 1, 1, 2, 2, 2, 2, 1, 1, 2, 2, 1, 1, 1, 2, 2, 4 ),
 ( 0.000000000000000000, 0.06250000000000000000, 0.09374999999999988898, 0.1249999999999997780, 0.1875000000000000000, 0.2187499999999997780, 0.2343749999999992784, 0.2499999999999987788, 0.3124999999999968359, 0.3437499999999963363, 0.3749999999999958367, 0.4374999999999958367, 0.4687499999999958367, 0.4843749999999952816, 0.4999999999999947264, 0.5624999999999947820, 0.6249999999999947820, 0.6874999999999947820, 0.7187499999999948930, 0.7343749999999948930, 0.7499999999999948930, 0.8124999999999954481, 0.8437499999999962252, 0.8593749999999964473, 0.8671874999999964473, 0.8749999999999964473, 1.000000000000000000 ),
 .UNSPECIFIED. ) ;
#6957=CARTESIAN_POINT ( 'NONE',  ( 21.50000000000000000, -6.938893903907228378E-15, 15.99999999999998579 ) ) ;
#6961=ADVANCED_FACE ( 'NONE', ( #4019 ), #5146, .T. ) ;
#6962=CARTESIAN_POINT ( 'NONE',  ( -8.500000000000003553, -218.0630240738404666, 44.76505905230349214 ) ) ;
#6964=ORIENTED_EDGE ( 'NONE', *, *, #1153, .F. ) ;
#6975=CARTESIAN_POINT ( 'NONE',  ( 10.18232950104899537, -221.3963574071737810, 72.83469615593526214 ) ) ;
#6976=CARTESIAN_POINT ( 'NONE',  ( 27.16044999292957840, -217.6494054747795417, 89.39435792273810932 ) ) ;
#6978=CARTESIAN_POINT ( 'NONE',  ( -13.64230087749234599, -110.6367035073516689, 38.63670350735182524 ) ) ;
#6982=FACE_OUTER_BOUND ( 'NONE', #1098, .T. ) ;
#6984=CARTESIAN_POINT ( 'NONE',  ( 21.40668666387986718, -218.0630240738405803, 82.00764644045258933 ) ) ;
#6985=CARTESIAN_POINT ( 'NONE',  ( 11.97238702448635728, -223.0630240738405234, 96.09122589815578408 ) ) ;
#6986=DIRECTION ( 'NONE',  ( 0.000000000000000000, -1.000000000000000000, -1.221245327087672392E-15 ) ) ;
#6990=CARTESIAN_POINT ( 'NONE',  ( -16.49999999999998934, -117.9145199278634522, 44.76505905230362714 ) ) ;
#7007=VECTOR ( 'NONE', #6794, 1000.000000000000000 ) ;
#7008=( BOUNDED_CURVE ( )  B_SPLINE_CURVE ( 3, ( #559, #1793, #1134, #4687 ),
 .UNSPECIFIED., .F., .T. ) 
 B_SPLINE_CURVE_WITH_KNOTS ( ( 4, 4 ),
 ( 3.926990816987240951, 4.712388980384689674 ),
 .UNSPECIFIED. ) 
 CURVE ( )  GEOMETRIC_REPRESENTATION_ITEM ( )  RATIONAL_B_SPLINE_CURVE ( ( 1.000000000000000000, 0.9492530216741910110, 0.9492530216741910110, 1.000000000000000000 ) ) 
 REPRESENTATION_ITEM ( '' )  );
#7010=CARTESIAN_POINT ( 'NONE',  ( 27.21559789597881007, -215.1711607728661022, 88.90143116695426784 ) ) ;
#7019=CARTESIAN_POINT ( 'NONE',  ( -29.77084236316893140, -74.27084236316864008, 47.27084236316875376 ) ) ;
#7024=CARTESIAN_POINT ( 'NONE',  ( -10.49999999999996803, -49.37258300203045280, -2.775557561562891351E-14 ) ) ;
#7034=VERTEX_POINT ( 'NONE', #4577 ) ;
#7036=CARTESIAN_POINT ( 'NONE',  ( -21.50000000000000000, -105.5631177942458265, 67.24940929526127320 ) ) ;
#7041=DIRECTION ( 'NONE',  ( -1.000000000000000000, 0.000000000000000000, -7.663350976776343357E-46 ) ) ;
#7042=ORIENTED_EDGE ( 'NONE', *, *, #1598, .F. ) ;
#7045=CARTESIAN_POINT ( 'NONE',  ( 10.25365409304695952, -218.1074892565148104, 95.21743140602106337 ) ) ;
#7046=ORIENTED_EDGE ( 'NONE', *, *, #37, .T. ) ;
#7051=VECTOR ( 'NONE', #2245, 1000.000000000000000 ) ;
#7061=EDGE_CURVE ( 'NONE', #3224, #5692, #3820, .T. ) ;
#7062=CARTESIAN_POINT ( 'NONE',  ( -16.49999999999996447, -6.938893903907228378E-15, 15.99999999999998579 ) ) ;
#7067=DIRECTION ( 'NONE',  ( 3.503246160812043455E-46, 0.7071067811865485719, 0.7071067811865464625 ) ) ;
#7074=CARTESIAN_POINT ( 'NONE',  ( -10.49999999999996980, 16.00000000000012079, -15.99999999999995914 ) ) ;
#7090=CARTESIAN_POINT ( 'NONE',  ( 17.75121803101545481, -218.1074892565148389, 95.21743140602129074 ) ) ;
#7100=CARTESIAN_POINT ( 'NONE',  ( -13.64230087749234599, -65.63670350735179682, 38.63670350735190340 ) ) ;
#7110=CARTESIAN_POINT ( 'NONE',  ( -10.49999999999997513, -59.26953873475991230, 32.26953873476001888 ) ) ;
#7113=ORIENTED_EDGE ( 'NONE', *, *, #1165, .T. ) ;
#7121=ORIENTED_EDGE ( 'NONE', *, *, #2605, .T. ) ;
#7124=CARTESIAN_POINT ( 'NONE',  ( 10.25562355766779277, -223.0194114314941203, 73.26959217102397304 ) ) ;
#7136=CARTESIAN_POINT ( 'NONE',  ( 11.01479902034195746, -218.0630240738405234, 95.20959099461350661 ) ) ;
#7138=DIRECTION ( 'NONE',  ( -1.000000000000000000, 1.294224922628222493E-31, -1.078147950931789264E-16 ) ) ;
#7139=VECTOR ( 'NONE', #6122, 1000.000000000000000 ) ;
#7140=LINE ( 'NONE', #3685, #1808 ) ;
#7142=DIRECTION ( 'NONE',  ( 0.000000000000000000, 1.301042606982600785E-15, -1.000000000000000000 ) ) ;
#7145=STYLED_ITEM('',(#7631),#1202);
#7148=ORIENTED_EDGE ( 'NONE', *, *, #7404, .F. ) ;
#7151=AXIS2_PLACEMENT_3D ( 'NONE', #6962, #5733, #2308 ) ;
#7152=DIRECTION ( 'NONE',  ( 0.5773502691896311712, 0.5773502691896222894, -0.5773502691896238437 ) ) ;
#7154=DIRECTION ( 'NONE',  ( 7.623657272262517133E-17, 0.7071067811865465735, -0.7071067811865485719 ) ) ;
#7159=ORIENTED_EDGE ( 'NONE', *, *, #1851, .T. ) ;
#7161=CARTESIAN_POINT ( 'NONE',  ( 10.50256896896200409, -228.4878731603044741, 74.73486207509921542 ) ) ;
#7167=EDGE_CURVE ( 'NONE', #4378, #628, #5688, .T. ) ;
#7186=EDGE_CURVE ( 'NONE', #2809, #4344, #148, .T. ) ;
#7190=AXIS2_PLACEMENT_3D ( 'NONE', #5677, #2745, #5105 ) ;
#7200=CARTESIAN_POINT ( 'NONE',  ( 17.82928583850155135, -228.1620966263573393, 74.64757051591656989 ) ) ;
#7204=FACE_BOUND ( 'NONE', #4903, .T. ) ;
#7208=ADVANCED_BREP_SHAPE_REPRESENTATION ( '', ( #1202, #1914 ), #5724 ) ;
#7211=VECTOR ( 'NONE', #3329, 1000.000000000000000 ) ;
#7219=LINE ( 'NONE', #1092, #5473 ) ;
#7237=EDGE_CURVE ( 'NONE', #5235, #3401, #4074, .T. ) ;
#7240=CARTESIAN_POINT ( 'NONE',  ( -10.49999999999996803, 0.000000000000000000, 0.000000000000000000 ) ) ;
#7245=VECTOR ( 'NONE', #6986, 1000.000000000000000 ) ;
#7248=ORIENTED_EDGE ( 'NONE', *, *, #1947, .T. ) ;
#7262=EDGE_CURVE ( 'NONE', #2069, #2279, #6128, .T. ) ;
#7263=CIRCLE ( 'NONE', #1479, 5.999999999999999112 ) ;
#7266=LINE ( 'NONE', #6691, #2851 ) ;
#7269=VERTEX_POINT ( 'NONE', #2949 ) ;
#7271=CIRCLE ( 'NONE', #3962, 6.000000000000000000 ) ;
#7273=CARTESIAN_POINT ( 'NONE',  ( 26.99871551551808579, -227.2977332969690281, 80.10323607719463723 ) ) ;
#7287=ORIENTED_EDGE ( 'NONE', *, *, #4295, .T. ) ;
#7294=CARTESIAN_POINT ( 'NONE',  ( -12.50000000000001066, -214.0630240738404382, 96.09122589815579829 ) ) ;
#7316=DIRECTION ( 'NONE',  ( 1.000000000000000000, -4.067564042545842122E-31, 3.379803290564626122E-16 ) ) ;
#7322=ORIENTED_EDGE ( 'NONE', *, *, #3130, .F. ) ;
#7324=DIRECTION ( 'NONE',  ( -1.000000000000000000, 0.000000000000000000, -7.663350976776343357E-46 ) ) ;
#7329=ORIENTED_EDGE ( 'NONE', *, *, #1342, .F. ) ;
#7338=ADVANCED_FACE ( 'NONE', ( #3179 ), #4381, .F. ) ;
#7344=ORIENTED_EDGE ( 'NONE', *, *, #1927, .F. ) ;
#7351=ADVANCED_FACE ( 'NONE', ( #861 ), #2597, .T. ) ;
#7356=PLANE ( 'NONE',  #4069 ) ;
#7377=DIRECTION ( 'NONE',  ( -2.627434620609033175E-46, 0.7071067811865464625, -0.7071067811865486830 ) ) ;
#7384=CARTESIAN_POINT ( 'NONE',  ( -13.35769912250762559, -110.3978942797115508, 38.39789427971171420 ) ) ;
#7393=FACE_OUTER_BOUND ( 'NONE', #6416, .T. ) ;
#7404=EDGE_CURVE ( 'NONE', #578, #3560, #3176, .T. ) ;
#7415=CIRCLE ( 'NONE', #4106, 7.999999999999986677 ) ;
#7423=CARTESIAN_POINT ( 'NONE',  ( 10.25759302228802738, -223.0630240738404382, 73.28127814332047762 ) ) ;
#7424=ORIENTED_EDGE ( 'NONE', *, *, #7262, .F. ) ;
#7456=( BOUNDED_CURVE ( )  B_SPLINE_CURVE ( 3, ( #3128, #5484, #3243, #212 ),
 .UNSPECIFIED., .F., .T. ) 
 B_SPLINE_CURVE_WITH_KNOTS ( ( 4, 4 ),
 ( 3.141592653589793116, 4.712388980384689674 ),
 .UNSPECIFIED. ) 
 CURVE ( )  GEOMETRIC_REPRESENTATION_ITEM ( )  RATIONAL_B_SPLINE_CURVE ( ( 1.000000000000000000, 0.8047378541243649375, 0.8047378541243649375, 1.000000000000000000 ) ) 
 REPRESENTATION_ITEM ( '' )  );
#7457=EDGE_CURVE ( 'NONE', #2279, #2955, #7219, .T. ) ;
#7458=DIRECTION ( 'NONE',  ( 7.006492321624086910E-46, -1.221245327087672392E-15, 1.000000000000000000 ) ) ;
#7459=VECTOR ( 'NONE', #1869, 1000.000000000000000 ) ;
#7478=CARTESIAN_POINT ( 'NONE',  ( 21.50000000000000000, -125.0933926253236308, 30.46597562735434295 ) ) ;
#7482=CARTESIAN_POINT ( 'NONE',  ( 15.24761270482150266, -223.0630240738404950, 74.45713762291202897 ) ) ;
#7485=( BOUNDED_CURVE ( )  B_SPLINE_CURVE ( 3, ( #3469, #3398, #2771, #3437 ),
 .UNSPECIFIED., .F., .T. ) 
 B_SPLINE_CURVE_WITH_KNOTS ( ( 4, 4 ),
 ( 0.7853981633974486121, 1.570796326794896558 ),
 .UNSPECIFIED. ) 
 CURVE ( )  GEOMETRIC_REPRESENTATION_ITEM ( )  RATIONAL_B_SPLINE_CURVE ( ( 1.000000000000000000, 0.9492530216741912330, 0.9492530216741912330, 1.000000000000000000 ) ) 
 REPRESENTATION_ITEM ( '' )  );
#7488=CARTESIAN_POINT ( 'NONE',  ( 14.60602998236824845, -218.0630240738405803, 72.92213505621988645 ) ) ;
#7491=DIRECTION ( 'NONE',  ( -1.084202172485504681E-16, 0.000000000000000000, 1.000000000000000000 ) ) ;
#7494=ORIENTED_EDGE ( 'NONE', *, *, #2120, .F. ) ;
#7506=CARTESIAN_POINT ( 'NONE',  ( 27.12317295347672541, -219.3245666396718434, 89.72755010419724897 ) ) ;
#7514=EDGE_CURVE ( 'NONE', #6147, #3224, #3948, .T. ) ;
#7515=DIRECTION ( 'NONE',  ( 0.000000000000000000, 0.000000000000000000, 1.000000000000000000 ) ) ;
#7527=CARTESIAN_POINT ( 'NONE',  ( -10.49999999999997513, -39.68629150101521219, 16.00000000000001421 ) ) ;
#7542=CARTESIAN_POINT ( 'NONE',  ( 10.17910001414514731, -216.4242598635583192, 94.92063264932131972 ) ) ;
#7543=ORIENTED_EDGE ( 'NONE', *, *, #7237, .T. ) ;
#7545=EDGE_CURVE ( 'NONE', #6433, #7034, #309, .T. ) ;
#7550=VERTEX_POINT ( 'NONE', #2217 ) ;
#7554=CARTESIAN_POINT ( 'NONE',  ( -16.49999999999996447, -39.68629150101521219, 16.00000000000001421 ) ) ;
#7566=DIRECTION ( 'NONE',  ( -1.381786968815111140E-76, 1.000000000000000000, 1.221245327087672392E-15 ) ) ;
#7570=ORIENTED_EDGE ( 'NONE', *, *, #2605, .F. ) ;
#7581=VERTEX_POINT ( 'NONE', #1286 ) ;
#7583=CARTESIAN_POINT ( 'NONE',  ( 10.48785751550376766, -223.3951688904015782, 96.14979199081797390 ) ) ;
#7593=CARTESIAN_POINT ( 'NONE',  ( 21.10457873213769986, -218.0630240738405234, 80.54341422479362222 ) ) ;
#7625=COLOUR_RGB('Sky Blue',0.24,0.69,0.87);
#7626=FILL_AREA_STYLE_COLOUR('',#7625);
#7627=FILL_AREA_STYLE('',(#7626));
#7628=SURFACE_STYLE_FILL_AREA(#7627);
#7629=SURFACE_SIDE_STYLE('',(#7628));
#7630=SURFACE_STYLE_USAGE(.BOTH.,#7629);
#7631=PRESENTATION_STYLE_ASSIGNMENT((#7630));
ENDSEC;
END-ISO-10303-21;
